ISO-10303-21;
HEADER;
/* Generated by software containing ST-Developer
 * from STEP Tools, Inc. (www.steptools.com) 
 */

FILE_DESCRIPTION(
/* description */ (''),
/* implementation_level */ '2;1');

FILE_NAME(
/* name */ 'Moving_Carriage_02.step',
/* time_stamp */ '2026-10-22T13:39:42+06:00',
/* author */ (''),
/* organization */ (''),
/* preprocessor_version */ 'ST-DEVELOPER v20.2',
/* originating_system */ 'Autodesk Translation Framework v15.15.0.0',
/* authorisation */ '');

FILE_SCHEMA (('AUTOMOTIVE_DESIGN { 1 0 10303 214 3 1 1 }'));
ENDSEC;

DATA;
#10=MECHANICAL_DESIGN_GEOMETRIC_PRESENTATION_REPRESENTATION('',(#309),#17836);
#133=SPHERICAL_SURFACE('',#9947,0.500000000000025);
#134=SPHERICAL_SURFACE('',#9951,0.500000000000005);
#135=SPHERICAL_SURFACE('',#9977,0.500000000000007);
#136=SPHERICAL_SURFACE('',#9982,0.499999999999998);
#137=SPHERICAL_SURFACE('',#9987,0.500000000000007);
#138=SPHERICAL_SURFACE('',#9991,0.500000000000007);
#139=SPHERICAL_SURFACE('',#9996,0.500000000000007);
#140=SPHERICAL_SURFACE('',#10001,0.500000000000007);
#141=SPHERICAL_SURFACE('',#10006,0.500000000000007);
#142=SPHERICAL_SURFACE('',#10010,0.500000000000007);
#143=SPHERICAL_SURFACE('',#10021,0.500000000000007);
#144=SPHERICAL_SURFACE('',#10030,0.500000000000007);
#145=SPHERICAL_SURFACE('',#10034,0.500000000000007);
#146=SPHERICAL_SURFACE('',#10039,0.499999999999998);
#147=SPHERICAL_SURFACE('',#10043,0.500000000000007);
#148=SPHERICAL_SURFACE('',#10047,0.499999999999998);
#219=TOROIDAL_SURFACE('',#9955,1.,0.5);
#220=TOROIDAL_SURFACE('',#9961,1.,0.500000000000002);
#221=TOROIDAL_SURFACE('',#9966,0.999999999999996,0.499999999999998);
#222=TOROIDAL_SURFACE('',#9971,1.,0.499999999999998);
#223=TOROIDAL_SURFACE('',#10015,0.999999999999999,0.499999999999998);
#224=TOROIDAL_SURFACE('',#10025,1.,0.499999999999998);
#225=TOROIDAL_SURFACE('',#10051,0.999999999999996,0.499999999999998);
#226=TOROIDAL_SURFACE('',#10058,1.00000000000001,0.500000000000007);
#289=SHAPE_REPRESENTATION_RELATIONSHIP('SRR','None',#17876,#299);
#299=ADVANCED_BREP_SHAPE_REPRESENTATION('',(#319),#17828);
#309=STYLED_ITEM('',(#17966),#319);
#319=MANIFOLD_SOLID_BREP('Moving_Carriage_02',#9630);
#368=CYLINDRICAL_SURFACE('',#9933,6.);
#369=CYLINDRICAL_SURFACE('',#9936,6.);
#370=CYLINDRICAL_SURFACE('',#9940,6.);
#371=CYLINDRICAL_SURFACE('',#9944,6.);
#372=CYLINDRICAL_SURFACE('',#9960,0.5);
#373=CYLINDRICAL_SURFACE('',#9976,0.5);
#374=CYLINDRICAL_SURFACE('',#9981,0.5);
#375=CYLINDRICAL_SURFACE('',#9986,0.5);
#376=CYLINDRICAL_SURFACE('',#9995,0.5);
#377=CYLINDRICAL_SURFACE('',#10000,0.5);
#378=CYLINDRICAL_SURFACE('',#10005,0.5);
#379=CYLINDRICAL_SURFACE('',#10014,0.5);
#380=CYLINDRICAL_SURFACE('',#10020,0.5);
#381=CYLINDRICAL_SURFACE('',#10038,0.5);
#382=CYLINDRICAL_SURFACE('',#10056,0.5);
#383=CYLINDRICAL_SURFACE('',#10057,0.5);
#384=CYLINDRICAL_SURFACE('',#10063,0.5);
#385=CYLINDRICAL_SURFACE('',#10064,0.5);
#386=CYLINDRICAL_SURFACE('',#10065,0.5);
#387=CYLINDRICAL_SURFACE('',#10066,0.5);
#388=CYLINDRICAL_SURFACE('',#10067,0.5);
#389=CYLINDRICAL_SURFACE('',#10068,0.5);
#390=CYLINDRICAL_SURFACE('',#10069,0.5);
#391=CYLINDRICAL_SURFACE('',#10070,0.5);
#392=CYLINDRICAL_SURFACE('',#10071,0.5);
#393=CYLINDRICAL_SURFACE('',#10072,0.5);
#394=CYLINDRICAL_SURFACE('',#10073,0.5);
#395=CYLINDRICAL_SURFACE('',#10074,0.5);
#396=CYLINDRICAL_SURFACE('',#10075,0.5);
#397=CYLINDRICAL_SURFACE('',#10076,0.5);
#398=CYLINDRICAL_SURFACE('',#10077,0.5);
#399=CYLINDRICAL_SURFACE('',#10078,0.5);
#400=CYLINDRICAL_SURFACE('',#10079,0.5);
#401=CYLINDRICAL_SURFACE('',#10080,0.5);
#402=CYLINDRICAL_SURFACE('',#10081,0.5);
#403=CYLINDRICAL_SURFACE('',#10082,0.5);
#404=CYLINDRICAL_SURFACE('',#10083,0.5);
#405=CYLINDRICAL_SURFACE('',#10084,0.5);
#406=CYLINDRICAL_SURFACE('',#10085,0.5);
#407=CYLINDRICAL_SURFACE('',#10086,0.5);
#743=LINE('',#14662,#1408);
#744=LINE('',#14668,#1409);
#745=LINE('',#14675,#1410);
#746=LINE('',#14682,#1411);
#747=LINE('',#14708,#1412);
#748=LINE('',#14709,#1413);
#749=LINE('',#14738,#1414);
#750=LINE('',#14739,#1415);
#751=LINE('',#14748,#1416);
#752=LINE('',#14749,#1417);
#753=LINE('',#14758,#1418);
#754=LINE('',#14759,#1419);
#755=LINE('',#14775,#1420);
#756=LINE('',#14776,#1421);
#757=LINE('',#14785,#1422);
#758=LINE('',#14786,#1423);
#759=LINE('',#14795,#1424);
#760=LINE('',#14796,#1425);
#761=LINE('',#14812,#1426);
#762=LINE('',#14813,#1427);
#763=LINE('',#14824,#1428);
#764=LINE('',#14825,#1429);
#765=LINE('',#14857,#1430);
#766=LINE('',#14858,#1431);
#767=LINE('',#14890,#1432);
#768=LINE('',#14891,#1433);
#769=LINE('',#14893,#1434);
#770=LINE('',#14894,#1435);
#771=LINE('',#14905,#1436);
#772=LINE('',#14906,#1437);
#773=LINE('',#14908,#1438);
#774=LINE('',#14909,#1439);
#775=LINE('',#14911,#1440);
#776=LINE('',#14912,#1441);
#777=LINE('',#14914,#1442);
#778=LINE('',#14915,#1443);
#779=LINE('',#14917,#1444);
#780=LINE('',#14918,#1445);
#781=LINE('',#14920,#1446);
#782=LINE('',#14921,#1447);
#783=LINE('',#14923,#1448);
#784=LINE('',#14924,#1449);
#785=LINE('',#14926,#1450);
#786=LINE('',#14927,#1451);
#787=LINE('',#14929,#1452);
#788=LINE('',#14930,#1453);
#789=LINE('',#14932,#1454);
#790=LINE('',#14933,#1455);
#791=LINE('',#14935,#1456);
#792=LINE('',#14936,#1457);
#793=LINE('',#14938,#1458);
#794=LINE('',#14939,#1459);
#795=LINE('',#14941,#1460);
#796=LINE('',#14942,#1461);
#797=LINE('',#14944,#1462);
#798=LINE('',#14945,#1463);
#799=LINE('',#14947,#1464);
#800=LINE('',#14948,#1465);
#801=LINE('',#14950,#1466);
#802=LINE('',#14951,#1467);
#803=LINE('',#14953,#1468);
#804=LINE('',#14954,#1469);
#805=LINE('',#14956,#1470);
#806=LINE('',#14957,#1471);
#807=LINE('',#14959,#1472);
#808=LINE('',#14960,#1473);
#809=LINE('',#14962,#1474);
#810=LINE('',#14963,#1475);
#811=LINE('',#14965,#1476);
#812=LINE('',#14966,#1477);
#813=LINE('',#14968,#1478);
#814=LINE('',#14969,#1479);
#815=LINE('',#14971,#1480);
#816=LINE('',#14972,#1481);
#817=LINE('',#14974,#1482);
#818=LINE('',#14975,#1483);
#1408=VECTOR('',#11507,6.);
#1409=VECTOR('',#11514,6.);
#1410=VECTOR('',#11523,6.);
#1411=VECTOR('',#11532,6.);
#1412=VECTOR('',#11563,10.);
#1413=VECTOR('',#11564,10.);
#1414=VECTOR('',#11597,10.);
#1415=VECTOR('',#11598,10.);
#1416=VECTOR('',#11609,10.);
#1417=VECTOR('',#11610,10.);
#1418=VECTOR('',#11621,10.);
#1419=VECTOR('',#11622,10.);
#1420=VECTOR('',#11641,10.);
#1421=VECTOR('',#11642,10.);
#1422=VECTOR('',#11653,10.);
#1423=VECTOR('',#11654,10.);
#1424=VECTOR('',#11665,10.);
#1425=VECTOR('',#11666,10.);
#1426=VECTOR('',#11685,10.);
#1427=VECTOR('',#11686,10.);
#1428=VECTOR('',#11699,10.);
#1429=VECTOR('',#11700,10.);
#1430=VECTOR('',#11737,10.);
#1431=VECTOR('',#11738,10.);
#1432=VECTOR('',#11775,10.);
#1433=VECTOR('',#11776,10.);
#1434=VECTOR('',#11779,10.);
#1435=VECTOR('',#11780,10.);
#1436=VECTOR('',#11793,10.);
#1437=VECTOR('',#11794,10.);
#1438=VECTOR('',#11797,10.);
#1439=VECTOR('',#11798,10.);
#1440=VECTOR('',#11801,10.);
#1441=VECTOR('',#11802,10.);
#1442=VECTOR('',#11805,10.);
#1443=VECTOR('',#11806,10.);
#1444=VECTOR('',#11809,10.);
#1445=VECTOR('',#11810,10.);
#1446=VECTOR('',#11813,10.);
#1447=VECTOR('',#11814,10.);
#1448=VECTOR('',#11817,10.);
#1449=VECTOR('',#11818,10.);
#1450=VECTOR('',#11821,10.);
#1451=VECTOR('',#11822,10.);
#1452=VECTOR('',#11825,10.);
#1453=VECTOR('',#11826,10.);
#1454=VECTOR('',#11829,10.);
#1455=VECTOR('',#11830,10.);
#1456=VECTOR('',#11833,10.);
#1457=VECTOR('',#11834,10.);
#1458=VECTOR('',#11837,10.);
#1459=VECTOR('',#11838,10.);
#1460=VECTOR('',#11841,10.);
#1461=VECTOR('',#11842,10.);
#1462=VECTOR('',#11845,10.);
#1463=VECTOR('',#11846,10.);
#1464=VECTOR('',#11849,10.);
#1465=VECTOR('',#11850,10.);
#1466=VECTOR('',#11853,10.);
#1467=VECTOR('',#11854,10.);
#1468=VECTOR('',#11857,10.);
#1469=VECTOR('',#11858,10.);
#1470=VECTOR('',#11861,10.);
#1471=VECTOR('',#11862,10.);
#1472=VECTOR('',#11865,10.);
#1473=VECTOR('',#11866,10.);
#1474=VECTOR('',#11869,10.);
#1475=VECTOR('',#11870,10.);
#1476=VECTOR('',#11873,10.);
#1477=VECTOR('',#11874,10.);
#1478=VECTOR('',#11877,10.);
#1479=VECTOR('',#11878,10.);
#1480=VECTOR('',#11881,10.);
#1481=VECTOR('',#11882,10.);
#1482=VECTOR('',#11885,10.);
#1483=VECTOR('',#11886,10.);
#1975=FACE_BOUND('',#2801,.T.);
#1976=FACE_BOUND('',#2802,.T.);
#1977=FACE_BOUND('',#2809,.T.);
#1978=FACE_BOUND('',#2810,.T.);
#1979=FACE_BOUND('',#2811,.T.);
#1980=FACE_BOUND('',#2812,.T.);
#2117=FACE_OUTER_BOUND('',#2732,.T.);
#2118=FACE_OUTER_BOUND('',#2733,.T.);
#2119=FACE_OUTER_BOUND('',#2734,.T.);
#2120=FACE_OUTER_BOUND('',#2735,.T.);
#2121=FACE_OUTER_BOUND('',#2736,.T.);
#2122=FACE_OUTER_BOUND('',#2737,.T.);
#2123=FACE_OUTER_BOUND('',#2738,.T.);
#2124=FACE_OUTER_BOUND('',#2739,.T.);
#2125=FACE_OUTER_BOUND('',#2740,.T.);
#2126=FACE_OUTER_BOUND('',#2741,.T.);
#2127=FACE_OUTER_BOUND('',#2742,.T.);
#2128=FACE_OUTER_BOUND('',#2743,.T.);
#2129=FACE_OUTER_BOUND('',#2744,.T.);
#2130=FACE_OUTER_BOUND('',#2745,.T.);
#2131=FACE_OUTER_BOUND('',#2746,.T.);
#2132=FACE_OUTER_BOUND('',#2747,.T.);
#2133=FACE_OUTER_BOUND('',#2748,.T.);
#2134=FACE_OUTER_BOUND('',#2749,.T.);
#2135=FACE_OUTER_BOUND('',#2750,.T.);
#2136=FACE_OUTER_BOUND('',#2751,.T.);
#2137=FACE_OUTER_BOUND('',#2752,.T.);
#2138=FACE_OUTER_BOUND('',#2753,.T.);
#2139=FACE_OUTER_BOUND('',#2754,.T.);
#2140=FACE_OUTER_BOUND('',#2755,.T.);
#2141=FACE_OUTER_BOUND('',#2756,.T.);
#2142=FACE_OUTER_BOUND('',#2757,.T.);
#2143=FACE_OUTER_BOUND('',#2758,.T.);
#2144=FACE_OUTER_BOUND('',#2759,.T.);
#2145=FACE_OUTER_BOUND('',#2760,.T.);
#2146=FACE_OUTER_BOUND('',#2761,.T.);
#2147=FACE_OUTER_BOUND('',#2762,.T.);
#2148=FACE_OUTER_BOUND('',#2763,.T.);
#2149=FACE_OUTER_BOUND('',#2764,.T.);
#2150=FACE_OUTER_BOUND('',#2765,.T.);
#2151=FACE_OUTER_BOUND('',#2766,.T.);
#2152=FACE_OUTER_BOUND('',#2767,.T.);
#2153=FACE_OUTER_BOUND('',#2768,.T.);
#2154=FACE_OUTER_BOUND('',#2769,.T.);
#2155=FACE_OUTER_BOUND('',#2770,.T.);
#2156=FACE_OUTER_BOUND('',#2771,.T.);
#2157=FACE_OUTER_BOUND('',#2772,.T.);
#2158=FACE_OUTER_BOUND('',#2773,.T.);
#2159=FACE_OUTER_BOUND('',#2774,.T.);
#2160=FACE_OUTER_BOUND('',#2775,.T.);
#2161=FACE_OUTER_BOUND('',#2776,.T.);
#2162=FACE_OUTER_BOUND('',#2777,.T.);
#2163=FACE_OUTER_BOUND('',#2778,.T.);
#2164=FACE_OUTER_BOUND('',#2779,.T.);
#2165=FACE_OUTER_BOUND('',#2780,.T.);
#2166=FACE_OUTER_BOUND('',#2781,.T.);
#2167=FACE_OUTER_BOUND('',#2782,.T.);
#2168=FACE_OUTER_BOUND('',#2783,.T.);
#2169=FACE_OUTER_BOUND('',#2784,.T.);
#2170=FACE_OUTER_BOUND('',#2785,.T.);
#2171=FACE_OUTER_BOUND('',#2786,.T.);
#2172=FACE_OUTER_BOUND('',#2787,.T.);
#2173=FACE_OUTER_BOUND('',#2788,.T.);
#2174=FACE_OUTER_BOUND('',#2789,.T.);
#2175=FACE_OUTER_BOUND('',#2790,.T.);
#2176=FACE_OUTER_BOUND('',#2791,.T.);
#2177=FACE_OUTER_BOUND('',#2792,.T.);
#2178=FACE_OUTER_BOUND('',#2793,.T.);
#2179=FACE_OUTER_BOUND('',#2794,.T.);
#2180=FACE_OUTER_BOUND('',#2795,.T.);
#2181=FACE_OUTER_BOUND('',#2796,.T.);
#2182=FACE_OUTER_BOUND('',#2797,.T.);
#2183=FACE_OUTER_BOUND('',#2798,.T.);
#2184=FACE_OUTER_BOUND('',#2799,.T.);
#2185=FACE_OUTER_BOUND('',#2800,.T.);
#2186=FACE_OUTER_BOUND('',#2803,.T.);
#2187=FACE_OUTER_BOUND('',#2804,.T.);
#2188=FACE_OUTER_BOUND('',#2805,.T.);
#2189=FACE_OUTER_BOUND('',#2806,.T.);
#2190=FACE_OUTER_BOUND('',#2807,.T.);
#2191=FACE_OUTER_BOUND('',#2808,.T.);
#2192=FACE_OUTER_BOUND('',#2813,.T.);
#2193=FACE_OUTER_BOUND('',#2814,.T.);
#2194=FACE_OUTER_BOUND('',#2815,.T.);
#2195=FACE_OUTER_BOUND('',#2816,.T.);
#2196=FACE_OUTER_BOUND('',#2817,.T.);
#2732=EDGE_LOOP('',(#6489,#6490,#6491,#6492));
#2733=EDGE_LOOP('',(#6493,#6494,#6495,#6496));
#2734=EDGE_LOOP('',(#6497));
#2735=EDGE_LOOP('',(#6498,#6499,#6500,#6501));
#2736=EDGE_LOOP('',(#6502));
#2737=EDGE_LOOP('',(#6503,#6504,#6505,#6506));
#2738=EDGE_LOOP('',(#6507,#6508,#6509));
#2739=EDGE_LOOP('',(#6510,#6511,#6512));
#2740=EDGE_LOOP('',(#6513,#6514,#6515,#6516));
#2741=EDGE_LOOP('',(#6517,#6518,#6519,#6520));
#2742=EDGE_LOOP('',(#6521,#6522,#6523,#6524));
#2743=EDGE_LOOP('',(#6525,#6526,#6527,#6528));
#2744=EDGE_LOOP('',(#6529,#6530,#6531,#6532));
#2745=EDGE_LOOP('',(#6533,#6534,#6535,#6536));
#2746=EDGE_LOOP('',(#6537,#6538,#6539));
#2747=EDGE_LOOP('',(#6540,#6541,#6542,#6543));
#2748=EDGE_LOOP('',(#6544,#6545,#6546));
#2749=EDGE_LOOP('',(#6547,#6548,#6549,#6550));
#2750=EDGE_LOOP('',(#6551,#6552,#6553));
#2751=EDGE_LOOP('',(#6554,#6555,#6556));
#2752=EDGE_LOOP('',(#6557,#6558,#6559,#6560));
#2753=EDGE_LOOP('',(#6561,#6562,#6563));
#2754=EDGE_LOOP('',(#6564,#6565,#6566,#6567));
#2755=EDGE_LOOP('',(#6568,#6569,#6570));
#2756=EDGE_LOOP('',(#6571,#6572,#6573,#6574));
#2757=EDGE_LOOP('',(#6575,#6576,#6577));
#2758=EDGE_LOOP('',(#6578,#6579,#6580));
#2759=EDGE_LOOP('',(#6581,#6582,#6583,#6584));
#2760=EDGE_LOOP('',(#6585,#6586,#6587,#6588));
#2761=EDGE_LOOP('',(#6589,#6590,#6591,#6592));
#2762=EDGE_LOOP('',(#6593,#6594,#6595));
#2763=EDGE_LOOP('',(#6596,#6597,#6598,#6599));
#2764=EDGE_LOOP('',(#6600,#6601,#6602));
#2765=EDGE_LOOP('',(#6603,#6604,#6605));
#2766=EDGE_LOOP('',(#6606,#6607,#6608,#6609));
#2767=EDGE_LOOP('',(#6610,#6611,#6612));
#2768=EDGE_LOOP('',(#6613,#6614,#6615));
#2769=EDGE_LOOP('',(#6616,#6617,#6618));
#2770=EDGE_LOOP('',(#6619,#6620,#6621,#6622));
#2771=EDGE_LOOP('',(#6623,#6624,#6625,#6626));
#2772=EDGE_LOOP('',(#6627,#6628,#6629,#6630));
#2773=EDGE_LOOP('',(#6631,#6632,#6633,#6634));
#2774=EDGE_LOOP('',(#6635,#6636,#6637,#6638));
#2775=EDGE_LOOP('',(#6639,#6640,#6641,#6642));
#2776=EDGE_LOOP('',(#6643,#6644,#6645,#6646));
#2777=EDGE_LOOP('',(#6647,#6648,#6649,#6650));
#2778=EDGE_LOOP('',(#6651,#6652,#6653,#6654));
#2779=EDGE_LOOP('',(#6655,#6656,#6657,#6658));
#2780=EDGE_LOOP('',(#6659,#6660,#6661,#6662));
#2781=EDGE_LOOP('',(#6663,#6664,#6665,#6666));
#2782=EDGE_LOOP('',(#6667,#6668,#6669,#6670));
#2783=EDGE_LOOP('',(#6671,#6672,#6673,#6674));
#2784=EDGE_LOOP('',(#6675,#6676,#6677,#6678));
#2785=EDGE_LOOP('',(#6679,#6680,#6681,#6682));
#2786=EDGE_LOOP('',(#6683,#6684,#6685,#6686));
#2787=EDGE_LOOP('',(#6687,#6688,#6689,#6690));
#2788=EDGE_LOOP('',(#6691,#6692,#6693,#6694));
#2789=EDGE_LOOP('',(#6695,#6696,#6697,#6698));
#2790=EDGE_LOOP('',(#6699,#6700,#6701,#6702));
#2791=EDGE_LOOP('',(#6703,#6704,#6705,#6706));
#2792=EDGE_LOOP('',(#6707,#6708,#6709,#6710));
#2793=EDGE_LOOP('',(#6711,#6712,#6713,#6714));
#2794=EDGE_LOOP('',(#6715,#6716,#6717,#6718));
#2795=EDGE_LOOP('',(#6719,#6720,#6721,#6722));
#2796=EDGE_LOOP('',(#6723,#6724,#6725,#6726));
#2797=EDGE_LOOP('',(#6727,#6728,#6729,#6730));
#2798=EDGE_LOOP('',(#6731,#6732,#6733,#6734,#6735,#6736,#6737,#6738,#6739,
#6740,#6741,#6742,#6743,#6744,#6745,#6746));
#2799=EDGE_LOOP('',(#6747,#6748,#6749,#6750));
#2800=EDGE_LOOP('',(#6751,#6752,#6753,#6754));
#2801=EDGE_LOOP('',(#6755));
#2802=EDGE_LOOP('',(#6756));
#2803=EDGE_LOOP('',(#6757,#6758,#6759,#6760));
#2804=EDGE_LOOP('',(#6761,#6762,#6763,#6764));
#2805=EDGE_LOOP('',(#6765,#6766,#6767,#6768));
#2806=EDGE_LOOP('',(#6769,#6770,#6771,#6772));
#2807=EDGE_LOOP('',(#6773,#6774,#6775,#6776));
#2808=EDGE_LOOP('',(#6777,#6778,#6779,#6780));
#2809=EDGE_LOOP('',(#6781));
#2810=EDGE_LOOP('',(#6782));
#2811=EDGE_LOOP('',(#6783));
#2812=EDGE_LOOP('',(#6784));
#2813=EDGE_LOOP('',(#6785,#6786,#6787,#6788));
#2814=EDGE_LOOP('',(#6789,#6790,#6791,#6792));
#2815=EDGE_LOOP('',(#6793,#6794,#6795,#6796));
#2816=EDGE_LOOP('',(#6797,#6798,#6799,#6800));
#2817=EDGE_LOOP('',(#6801,#6802,#6803,#6804,#6805,#6806,#6807,#6808,#6809,
#6810,#6811,#6812,#6813,#6814,#6815,#6816));
#3396=CIRCLE('',#9934,6.);
#3397=CIRCLE('',#9935,6.);
#3398=CIRCLE('',#9937,6.);
#3399=CIRCLE('',#9938,6.);
#3400=CIRCLE('',#9941,6.);
#3401=CIRCLE('',#9942,6.);
#3402=CIRCLE('',#9945,6.);
#3403=CIRCLE('',#9946,6.);
#3404=CIRCLE('',#9948,0.499999999999999);
#3405=CIRCLE('',#9949,0.500000000000025);
#3406=CIRCLE('',#9950,0.499999999999998);
#3407=CIRCLE('',#9952,0.500000000000007);
#3408=CIRCLE('',#9953,0.500000000000005);
#3409=CIRCLE('',#9954,0.5);
#3410=CIRCLE('',#9956,0.499999999999998);
#3411=CIRCLE('',#9957,0.500000000000007);
#3412=CIRCLE('',#9958,0.999999999999996);
#3413=CIRCLE('',#9959,0.5);
#3414=CIRCLE('',#9962,1.);
#3415=CIRCLE('',#9963,0.500000000000002);
#3416=CIRCLE('',#9964,0.499999999999998);
#3417=CIRCLE('',#9965,0.500000000000007);
#3418=CIRCLE('',#9967,0.5);
#3419=CIRCLE('',#9968,0.500000000000007);
#3420=CIRCLE('',#9969,1.);
#3421=CIRCLE('',#9970,0.499999999999998);
#3422=CIRCLE('',#9972,1.00000000000001);
#3423=CIRCLE('',#9973,0.499999999999998);
#3424=CIRCLE('',#9974,0.499999999999999);
#3425=CIRCLE('',#9975,0.500000000000007);
#3426=CIRCLE('',#9978,0.5);
#3427=CIRCLE('',#9979,0.500000000000007);
#3428=CIRCLE('',#9980,0.499999999999999);
#3429=CIRCLE('',#9983,0.500000000000007);
#3430=CIRCLE('',#9984,0.499999999999998);
#3431=CIRCLE('',#9985,0.499999999999998);
#3432=CIRCLE('',#9988,0.499999999999999);
#3433=CIRCLE('',#9989,0.500000000000007);
#3434=CIRCLE('',#9990,0.5);
#3435=CIRCLE('',#9992,0.499999999999998);
#3436=CIRCLE('',#9993,0.500000000000007);
#3437=CIRCLE('',#9994,0.500000000000007);
#3438=CIRCLE('',#9997,0.5);
#3439=CIRCLE('',#9998,0.500000000000007);
#3440=CIRCLE('',#9999,0.499999999999998);
#3441=CIRCLE('',#10002,0.500000000000007);
#3442=CIRCLE('',#10003,0.500000000000007);
#3443=CIRCLE('',#10004,0.499999999999998);
#3444=CIRCLE('',#10007,0.499999999999998);
#3445=CIRCLE('',#10008,0.500000000000007);
#3446=CIRCLE('',#10009,0.499999999999999);
#3447=CIRCLE('',#10011,0.499999999999998);
#3448=CIRCLE('',#10012,0.500000000000007);
#3449=CIRCLE('',#10013,0.499999999999998);
#3450=CIRCLE('',#10016,0.499999999999998);
#3451=CIRCLE('',#10017,0.500000000000007);
#3452=CIRCLE('',#10018,0.999999999999996);
#3453=CIRCLE('',#10019,0.499999999999998);
#3454=CIRCLE('',#10022,0.499999999999998);
#3455=CIRCLE('',#10023,0.500000000000007);
#3456=CIRCLE('',#10024,0.499999999999998);
#3457=CIRCLE('',#10026,0.5);
#3458=CIRCLE('',#10027,0.500000000000007);
#3459=CIRCLE('',#10028,0.999999999999999);
#3460=CIRCLE('',#10029,0.499999999999998);
#3461=CIRCLE('',#10031,0.500000000000007);
#3462=CIRCLE('',#10032,0.500000000000007);
#3463=CIRCLE('',#10033,0.499999999999998);
#3464=CIRCLE('',#10035,0.499999999999998);
#3465=CIRCLE('',#10036,0.500000000000007);
#3466=CIRCLE('',#10037,0.500000000000007);
#3467=CIRCLE('',#10040,0.500000000000007);
#3468=CIRCLE('',#10041,0.499999999999998);
#3469=CIRCLE('',#10042,0.500000000000007);
#3470=CIRCLE('',#10044,0.499999999999998);
#3471=CIRCLE('',#10045,0.500000000000007);
#3472=CIRCLE('',#10046,0.499999999999998);
#3473=CIRCLE('',#10048,0.500000000000007);
#3474=CIRCLE('',#10049,0.499999999999998);
#3475=CIRCLE('',#10050,0.499999999999998);
#3476=CIRCLE('',#10052,0.499999999999998);
#3477=CIRCLE('',#10053,0.500000000000007);
#3478=CIRCLE('',#10054,1.00000000000001);
#3479=CIRCLE('',#10055,0.499999999999998);
#3480=CIRCLE('',#10059,0.499999999999998);
#3481=CIRCLE('',#10060,0.500000000000007);
#3482=CIRCLE('',#10061,0.999999999999996);
#3483=CIRCLE('',#10062,0.500000000000007);
#4044=VERTEX_POINT('',#14659);
#4045=VERTEX_POINT('',#14661);
#4046=VERTEX_POINT('',#14665);
#4047=VERTEX_POINT('',#14667);
#4048=VERTEX_POINT('',#14672);
#4049=VERTEX_POINT('',#14674);
#4050=VERTEX_POINT('',#14679);
#4051=VERTEX_POINT('',#14681);
#4052=VERTEX_POINT('',#14685);
#4053=VERTEX_POINT('',#14686);
#4054=VERTEX_POINT('',#14688);
#4055=VERTEX_POINT('',#14692);
#4056=VERTEX_POINT('',#14693);
#4057=VERTEX_POINT('',#14695);
#4058=VERTEX_POINT('',#14699);
#4059=VERTEX_POINT('',#14700);
#4060=VERTEX_POINT('',#14702);
#4061=VERTEX_POINT('',#14704);
#4062=VERTEX_POINT('',#14711);
#4063=VERTEX_POINT('',#14712);
#4064=VERTEX_POINT('',#14714);
#4065=VERTEX_POINT('',#14716);
#4066=VERTEX_POINT('',#14720);
#4067=VERTEX_POINT('',#14721);
#4068=VERTEX_POINT('',#14723);
#4069=VERTEX_POINT('',#14725);
#4070=VERTEX_POINT('',#14729);
#4071=VERTEX_POINT('',#14730);
#4072=VERTEX_POINT('',#14732);
#4073=VERTEX_POINT('',#14734);
#4074=VERTEX_POINT('',#14741);
#4075=VERTEX_POINT('',#14742);
#4076=VERTEX_POINT('',#14744);
#4077=VERTEX_POINT('',#14751);
#4078=VERTEX_POINT('',#14752);
#4079=VERTEX_POINT('',#14754);
#4080=VERTEX_POINT('',#14761);
#4081=VERTEX_POINT('',#14762);
#4082=VERTEX_POINT('',#14764);
#4083=VERTEX_POINT('',#14768);
#4084=VERTEX_POINT('',#14769);
#4085=VERTEX_POINT('',#14771);
#4086=VERTEX_POINT('',#14778);
#4087=VERTEX_POINT('',#14779);
#4088=VERTEX_POINT('',#14781);
#4089=VERTEX_POINT('',#14788);
#4090=VERTEX_POINT('',#14789);
#4091=VERTEX_POINT('',#14791);
#4092=VERTEX_POINT('',#14798);
#4093=VERTEX_POINT('',#14799);
#4094=VERTEX_POINT('',#14801);
#4095=VERTEX_POINT('',#14805);
#4096=VERTEX_POINT('',#14806);
#4097=VERTEX_POINT('',#14808);
#4098=VERTEX_POINT('',#14815);
#4099=VERTEX_POINT('',#14816);
#4100=VERTEX_POINT('',#14818);
#4101=VERTEX_POINT('',#14820);
#4102=VERTEX_POINT('',#14827);
#4103=VERTEX_POINT('',#14828);
#4104=VERTEX_POINT('',#14830);
#4105=VERTEX_POINT('',#14834);
#4106=VERTEX_POINT('',#14835);
#4107=VERTEX_POINT('',#14837);
#4108=VERTEX_POINT('',#14839);
#4109=VERTEX_POINT('',#14843);
#4110=VERTEX_POINT('',#14844);
#4111=VERTEX_POINT('',#14846);
#4112=VERTEX_POINT('',#14850);
#4113=VERTEX_POINT('',#14851);
#4114=VERTEX_POINT('',#14853);
#4115=VERTEX_POINT('',#14860);
#4116=VERTEX_POINT('',#14861);
#4117=VERTEX_POINT('',#14863);
#4118=VERTEX_POINT('',#14867);
#4119=VERTEX_POINT('',#14868);
#4120=VERTEX_POINT('',#14870);
#4121=VERTEX_POINT('',#14874);
#4122=VERTEX_POINT('',#14875);
#4123=VERTEX_POINT('',#14877);
#4124=VERTEX_POINT('',#14881);
#4125=VERTEX_POINT('',#14882);
#4126=VERTEX_POINT('',#14884);
#4127=VERTEX_POINT('',#14886);
#4128=VERTEX_POINT('',#14896);
#4129=VERTEX_POINT('',#14897);
#4130=VERTEX_POINT('',#14899);
#4131=VERTEX_POINT('',#14901);
#4915=EDGE_CURVE('',#4044,#4044,#3396,.T.);
#4916=EDGE_CURVE('',#4044,#4045,#743,.T.);
#4917=EDGE_CURVE('',#4045,#4045,#3397,.T.);
#4918=EDGE_CURVE('',#4046,#4046,#3398,.T.);
#4919=EDGE_CURVE('',#4046,#4047,#744,.T.);
#4920=EDGE_CURVE('',#4047,#4047,#3399,.T.);
#4921=EDGE_CURVE('',#4048,#4048,#3400,.T.);
#4922=EDGE_CURVE('',#4048,#4049,#745,.T.);
#4923=EDGE_CURVE('',#4049,#4049,#3401,.T.);
#4924=EDGE_CURVE('',#4050,#4050,#3402,.T.);
#4925=EDGE_CURVE('',#4050,#4051,#746,.T.);
#4926=EDGE_CURVE('',#4051,#4051,#3403,.T.);
#4927=EDGE_CURVE('',#4052,#4053,#3404,.F.);
#4928=EDGE_CURVE('',#4054,#4052,#3405,.F.);
#4929=EDGE_CURVE('',#4053,#4054,#3406,.F.);
#4930=EDGE_CURVE('',#4055,#4056,#3407,.F.);
#4931=EDGE_CURVE('',#4057,#4055,#3408,.F.);
#4932=EDGE_CURVE('',#4056,#4057,#3409,.F.);
#4933=EDGE_CURVE('',#4058,#4059,#3410,.F.);
#4934=EDGE_CURVE('',#4060,#4058,#3411,.T.);
#4935=EDGE_CURVE('',#4060,#4061,#3412,.T.);
#4936=EDGE_CURVE('',#4059,#4061,#3413,.T.);
#4937=EDGE_CURVE('',#4058,#4053,#747,.T.);
#4938=EDGE_CURVE('',#4054,#4060,#748,.T.);
#4939=EDGE_CURVE('',#4062,#4063,#3414,.T.);
#4940=EDGE_CURVE('',#4064,#4063,#3415,.T.);
#4941=EDGE_CURVE('',#4065,#4064,#3416,.F.);
#4942=EDGE_CURVE('',#4062,#4065,#3417,.T.);
#4943=EDGE_CURVE('',#4066,#4067,#3418,.F.);
#4944=EDGE_CURVE('',#4068,#4066,#3419,.T.);
#4945=EDGE_CURVE('',#4068,#4069,#3420,.T.);
#4946=EDGE_CURVE('',#4067,#4069,#3421,.T.);
#4947=EDGE_CURVE('',#4070,#4071,#3422,.T.);
#4948=EDGE_CURVE('',#4072,#4071,#3423,.T.);
#4949=EDGE_CURVE('',#4073,#4072,#3424,.F.);
#4950=EDGE_CURVE('',#4070,#4073,#3425,.T.);
#4951=EDGE_CURVE('',#4073,#4057,#749,.T.);
#4952=EDGE_CURVE('',#4055,#4070,#750,.T.);
#4953=EDGE_CURVE('',#4074,#4075,#3426,.F.);
#4954=EDGE_CURVE('',#4076,#4074,#3427,.F.);
#4955=EDGE_CURVE('',#4075,#4076,#3428,.F.);
#4956=EDGE_CURVE('',#4074,#4059,#751,.T.);
#4957=EDGE_CURVE('',#4061,#4076,#752,.T.);
#4958=EDGE_CURVE('',#4077,#4078,#3429,.F.);
#4959=EDGE_CURVE('',#4079,#4077,#3430,.F.);
#4960=EDGE_CURVE('',#4078,#4079,#3431,.F.);
#4961=EDGE_CURVE('',#4077,#4062,#753,.T.);
#4962=EDGE_CURVE('',#4065,#4079,#754,.T.);
#4963=EDGE_CURVE('',#4080,#4081,#3432,.F.);
#4964=EDGE_CURVE('',#4082,#4080,#3433,.F.);
#4965=EDGE_CURVE('',#4081,#4082,#3434,.F.);
#4966=EDGE_CURVE('',#4083,#4084,#3435,.F.);
#4967=EDGE_CURVE('',#4085,#4083,#3436,.F.);
#4968=EDGE_CURVE('',#4084,#4085,#3437,.F.);
#4969=EDGE_CURVE('',#4071,#4085,#755,.T.);
#4970=EDGE_CURVE('',#4083,#4072,#756,.T.);
#4971=EDGE_CURVE('',#4086,#4087,#3438,.F.);
#4972=EDGE_CURVE('',#4088,#4086,#3439,.F.);
#4973=EDGE_CURVE('',#4087,#4088,#3440,.F.);
#4974=EDGE_CURVE('',#4086,#4075,#757,.T.);
#4975=EDGE_CURVE('',#4076,#4088,#758,.T.);
#4976=EDGE_CURVE('',#4089,#4090,#3441,.F.);
#4977=EDGE_CURVE('',#4091,#4089,#3442,.F.);
#4978=EDGE_CURVE('',#4090,#4091,#3443,.F.);
#4979=EDGE_CURVE('',#4089,#4077,#759,.T.);
#4980=EDGE_CURVE('',#4078,#4091,#760,.T.);
#4981=EDGE_CURVE('',#4092,#4093,#3444,.F.);
#4982=EDGE_CURVE('',#4094,#4092,#3445,.F.);
#4983=EDGE_CURVE('',#4093,#4094,#3446,.F.);
#4984=EDGE_CURVE('',#4095,#4096,#3447,.F.);
#4985=EDGE_CURVE('',#4097,#4095,#3448,.F.);
#4986=EDGE_CURVE('',#4096,#4097,#3449,.F.);
#4987=EDGE_CURVE('',#4095,#4084,#761,.T.);
#4988=EDGE_CURVE('',#4085,#4097,#762,.T.);
#4989=EDGE_CURVE('',#4098,#4099,#3450,.F.);
#4990=EDGE_CURVE('',#4100,#4098,#3451,.T.);
#4991=EDGE_CURVE('',#4100,#4101,#3452,.T.);
#4992=EDGE_CURVE('',#4099,#4101,#3453,.T.);
#4993=EDGE_CURVE('',#4098,#4087,#763,.T.);
#4994=EDGE_CURVE('',#4088,#4100,#764,.T.);
#4995=EDGE_CURVE('',#4102,#4103,#3454,.F.);
#4996=EDGE_CURVE('',#4104,#4102,#3455,.F.);
#4997=EDGE_CURVE('',#4103,#4104,#3456,.F.);
#4998=EDGE_CURVE('',#4105,#4106,#3457,.F.);
#4999=EDGE_CURVE('',#4107,#4105,#3458,.T.);
#5000=EDGE_CURVE('',#4107,#4108,#3459,.T.);
#5001=EDGE_CURVE('',#4106,#4108,#3460,.T.);
#5002=EDGE_CURVE('',#4109,#4110,#3461,.F.);
#5003=EDGE_CURVE('',#4111,#4109,#3462,.F.);
#5004=EDGE_CURVE('',#4110,#4111,#3463,.F.);
#5005=EDGE_CURVE('',#4112,#4113,#3464,.F.);
#5006=EDGE_CURVE('',#4114,#4112,#3465,.F.);
#5007=EDGE_CURVE('',#4113,#4114,#3466,.F.);
#5008=EDGE_CURVE('',#4112,#4099,#765,.T.);
#5009=EDGE_CURVE('',#4101,#4114,#766,.T.);
#5010=EDGE_CURVE('',#4115,#4116,#3467,.F.);
#5011=EDGE_CURVE('',#4117,#4115,#3468,.F.);
#5012=EDGE_CURVE('',#4116,#4117,#3469,.F.);
#5013=EDGE_CURVE('',#4118,#4119,#3470,.F.);
#5014=EDGE_CURVE('',#4120,#4118,#3471,.F.);
#5015=EDGE_CURVE('',#4119,#4120,#3472,.F.);
#5016=EDGE_CURVE('',#4121,#4122,#3473,.F.);
#5017=EDGE_CURVE('',#4123,#4121,#3474,.F.);
#5018=EDGE_CURVE('',#4122,#4123,#3475,.F.);
#5019=EDGE_CURVE('',#4124,#4125,#3476,.F.);
#5020=EDGE_CURVE('',#4126,#4124,#3477,.T.);
#5021=EDGE_CURVE('',#4126,#4127,#3478,.T.);
#5022=EDGE_CURVE('',#4125,#4127,#3479,.T.);
#5023=EDGE_CURVE('',#4124,#4113,#767,.T.);
#5024=EDGE_CURVE('',#4114,#4126,#768,.T.);
#5025=EDGE_CURVE('',#4127,#4116,#769,.T.);
#5026=EDGE_CURVE('',#4117,#4125,#770,.T.);
#5027=EDGE_CURVE('',#4128,#4129,#3480,.F.);
#5028=EDGE_CURVE('',#4130,#4128,#3481,.T.);
#5029=EDGE_CURVE('',#4130,#4131,#3482,.T.);
#5030=EDGE_CURVE('',#4129,#4131,#3483,.T.);
#5031=EDGE_CURVE('',#4121,#4130,#771,.T.);
#5032=EDGE_CURVE('',#4128,#4123,#772,.T.);
#5033=EDGE_CURVE('',#4118,#4129,#773,.T.);
#5034=EDGE_CURVE('',#4131,#4120,#774,.T.);
#5035=EDGE_CURVE('',#4125,#4128,#775,.T.);
#5036=EDGE_CURVE('',#4129,#4124,#776,.T.);
#5037=EDGE_CURVE('',#4115,#4122,#777,.T.);
#5038=EDGE_CURVE('',#4123,#4117,#778,.T.);
#5039=EDGE_CURVE('',#4109,#4121,#779,.T.);
#5040=EDGE_CURVE('',#4122,#4111,#780,.T.);
#5041=EDGE_CURVE('',#4105,#4119,#781,.T.);
#5042=EDGE_CURVE('',#4120,#4107,#782,.T.);
#5043=EDGE_CURVE('',#4119,#4112,#783,.T.);
#5044=EDGE_CURVE('',#4113,#4118,#784,.T.);
#5045=EDGE_CURVE('',#4102,#4115,#785,.T.);
#5046=EDGE_CURVE('',#4116,#4104,#786,.T.);
#5047=EDGE_CURVE('',#4103,#4110,#787,.T.);
#5048=EDGE_CURVE('',#4111,#4102,#788,.T.);
#5049=EDGE_CURVE('',#4110,#4096,#789,.T.);
#5050=EDGE_CURVE('',#4097,#4109,#790,.T.);
#5051=EDGE_CURVE('',#4092,#4106,#791,.T.);
#5052=EDGE_CURVE('',#4108,#4094,#792,.T.);
#5053=EDGE_CURVE('',#4106,#4098,#793,.T.);
#5054=EDGE_CURVE('',#4099,#4105,#794,.T.);
#5055=EDGE_CURVE('',#4090,#4103,#795,.T.);
#5056=EDGE_CURVE('',#4104,#4089,#796,.T.);
#5057=EDGE_CURVE('',#4096,#4090,#797,.T.);
#5058=EDGE_CURVE('',#4091,#4095,#798,.T.);
#5059=EDGE_CURVE('',#4080,#4093,#799,.T.);
#5060=EDGE_CURVE('',#4094,#4082,#800,.T.);
#5061=EDGE_CURVE('',#4093,#4086,#801,.T.);
#5062=EDGE_CURVE('',#4087,#4092,#802,.T.);
#5063=EDGE_CURVE('',#4084,#4078,#803,.T.);
#5064=EDGE_CURVE('',#4079,#4083,#804,.T.);
#5065=EDGE_CURVE('',#4066,#4081,#805,.T.);
#5066=EDGE_CURVE('',#4082,#4068,#806,.T.);
#5067=EDGE_CURVE('',#4081,#4074,#807,.T.);
#5068=EDGE_CURVE('',#4075,#4080,#808,.T.);
#5069=EDGE_CURVE('',#4072,#4065,#809,.T.);
#5070=EDGE_CURVE('',#4064,#4073,#810,.T.);
#5071=EDGE_CURVE('',#4056,#4067,#811,.T.);
#5072=EDGE_CURVE('',#4069,#4055,#812,.T.);
#5073=EDGE_CURVE('',#4067,#4058,#813,.T.);
#5074=EDGE_CURVE('',#4059,#4066,#814,.T.);
#5075=EDGE_CURVE('',#4052,#4064,#815,.T.);
#5076=EDGE_CURVE('',#4063,#4054,#816,.T.);
#5077=EDGE_CURVE('',#4057,#4052,#817,.T.);
#5078=EDGE_CURVE('',#4053,#4056,#818,.T.);
#6489=ORIENTED_EDGE('',*,*,#4915,.F.);
#6490=ORIENTED_EDGE('',*,*,#4916,.T.);
#6491=ORIENTED_EDGE('',*,*,#4917,.F.);
#6492=ORIENTED_EDGE('',*,*,#4916,.F.);
#6493=ORIENTED_EDGE('',*,*,#4918,.F.);
#6494=ORIENTED_EDGE('',*,*,#4919,.T.);
#6495=ORIENTED_EDGE('',*,*,#4920,.T.);
#6496=ORIENTED_EDGE('',*,*,#4919,.F.);
#6497=ORIENTED_EDGE('',*,*,#4920,.F.);
#6498=ORIENTED_EDGE('',*,*,#4921,.F.);
#6499=ORIENTED_EDGE('',*,*,#4922,.T.);
#6500=ORIENTED_EDGE('',*,*,#4923,.T.);
#6501=ORIENTED_EDGE('',*,*,#4922,.F.);
#6502=ORIENTED_EDGE('',*,*,#4923,.F.);
#6503=ORIENTED_EDGE('',*,*,#4924,.F.);
#6504=ORIENTED_EDGE('',*,*,#4925,.T.);
#6505=ORIENTED_EDGE('',*,*,#4926,.F.);
#6506=ORIENTED_EDGE('',*,*,#4925,.F.);
#6507=ORIENTED_EDGE('',*,*,#4927,.F.);
#6508=ORIENTED_EDGE('',*,*,#4928,.F.);
#6509=ORIENTED_EDGE('',*,*,#4929,.F.);
#6510=ORIENTED_EDGE('',*,*,#4930,.F.);
#6511=ORIENTED_EDGE('',*,*,#4931,.F.);
#6512=ORIENTED_EDGE('',*,*,#4932,.F.);
#6513=ORIENTED_EDGE('',*,*,#4933,.F.);
#6514=ORIENTED_EDGE('',*,*,#4934,.F.);
#6515=ORIENTED_EDGE('',*,*,#4935,.T.);
#6516=ORIENTED_EDGE('',*,*,#4936,.F.);
#6517=ORIENTED_EDGE('',*,*,#4934,.T.);
#6518=ORIENTED_EDGE('',*,*,#4937,.T.);
#6519=ORIENTED_EDGE('',*,*,#4929,.T.);
#6520=ORIENTED_EDGE('',*,*,#4938,.T.);
#6521=ORIENTED_EDGE('',*,*,#4939,.T.);
#6522=ORIENTED_EDGE('',*,*,#4940,.F.);
#6523=ORIENTED_EDGE('',*,*,#4941,.F.);
#6524=ORIENTED_EDGE('',*,*,#4942,.F.);
#6525=ORIENTED_EDGE('',*,*,#4943,.F.);
#6526=ORIENTED_EDGE('',*,*,#4944,.F.);
#6527=ORIENTED_EDGE('',*,*,#4945,.T.);
#6528=ORIENTED_EDGE('',*,*,#4946,.F.);
#6529=ORIENTED_EDGE('',*,*,#4947,.T.);
#6530=ORIENTED_EDGE('',*,*,#4948,.F.);
#6531=ORIENTED_EDGE('',*,*,#4949,.F.);
#6532=ORIENTED_EDGE('',*,*,#4950,.F.);
#6533=ORIENTED_EDGE('',*,*,#4950,.T.);
#6534=ORIENTED_EDGE('',*,*,#4951,.T.);
#6535=ORIENTED_EDGE('',*,*,#4931,.T.);
#6536=ORIENTED_EDGE('',*,*,#4952,.T.);
#6537=ORIENTED_EDGE('',*,*,#4953,.F.);
#6538=ORIENTED_EDGE('',*,*,#4954,.F.);
#6539=ORIENTED_EDGE('',*,*,#4955,.F.);
#6540=ORIENTED_EDGE('',*,*,#4954,.T.);
#6541=ORIENTED_EDGE('',*,*,#4956,.T.);
#6542=ORIENTED_EDGE('',*,*,#4936,.T.);
#6543=ORIENTED_EDGE('',*,*,#4957,.T.);
#6544=ORIENTED_EDGE('',*,*,#4958,.F.);
#6545=ORIENTED_EDGE('',*,*,#4959,.F.);
#6546=ORIENTED_EDGE('',*,*,#4960,.F.);
#6547=ORIENTED_EDGE('',*,*,#4959,.T.);
#6548=ORIENTED_EDGE('',*,*,#4961,.T.);
#6549=ORIENTED_EDGE('',*,*,#4942,.T.);
#6550=ORIENTED_EDGE('',*,*,#4962,.T.);
#6551=ORIENTED_EDGE('',*,*,#4963,.F.);
#6552=ORIENTED_EDGE('',*,*,#4964,.F.);
#6553=ORIENTED_EDGE('',*,*,#4965,.F.);
#6554=ORIENTED_EDGE('',*,*,#4966,.F.);
#6555=ORIENTED_EDGE('',*,*,#4967,.F.);
#6556=ORIENTED_EDGE('',*,*,#4968,.F.);
#6557=ORIENTED_EDGE('',*,*,#4948,.T.);
#6558=ORIENTED_EDGE('',*,*,#4969,.T.);
#6559=ORIENTED_EDGE('',*,*,#4967,.T.);
#6560=ORIENTED_EDGE('',*,*,#4970,.T.);
#6561=ORIENTED_EDGE('',*,*,#4971,.F.);
#6562=ORIENTED_EDGE('',*,*,#4972,.F.);
#6563=ORIENTED_EDGE('',*,*,#4973,.F.);
#6564=ORIENTED_EDGE('',*,*,#4972,.T.);
#6565=ORIENTED_EDGE('',*,*,#4974,.T.);
#6566=ORIENTED_EDGE('',*,*,#4955,.T.);
#6567=ORIENTED_EDGE('',*,*,#4975,.T.);
#6568=ORIENTED_EDGE('',*,*,#4976,.F.);
#6569=ORIENTED_EDGE('',*,*,#4977,.F.);
#6570=ORIENTED_EDGE('',*,*,#4978,.F.);
#6571=ORIENTED_EDGE('',*,*,#4977,.T.);
#6572=ORIENTED_EDGE('',*,*,#4979,.T.);
#6573=ORIENTED_EDGE('',*,*,#4958,.T.);
#6574=ORIENTED_EDGE('',*,*,#4980,.T.);
#6575=ORIENTED_EDGE('',*,*,#4981,.F.);
#6576=ORIENTED_EDGE('',*,*,#4982,.F.);
#6577=ORIENTED_EDGE('',*,*,#4983,.F.);
#6578=ORIENTED_EDGE('',*,*,#4984,.F.);
#6579=ORIENTED_EDGE('',*,*,#4985,.F.);
#6580=ORIENTED_EDGE('',*,*,#4986,.F.);
#6581=ORIENTED_EDGE('',*,*,#4985,.T.);
#6582=ORIENTED_EDGE('',*,*,#4987,.T.);
#6583=ORIENTED_EDGE('',*,*,#4968,.T.);
#6584=ORIENTED_EDGE('',*,*,#4988,.T.);
#6585=ORIENTED_EDGE('',*,*,#4989,.F.);
#6586=ORIENTED_EDGE('',*,*,#4990,.F.);
#6587=ORIENTED_EDGE('',*,*,#4991,.T.);
#6588=ORIENTED_EDGE('',*,*,#4992,.F.);
#6589=ORIENTED_EDGE('',*,*,#4990,.T.);
#6590=ORIENTED_EDGE('',*,*,#4993,.T.);
#6591=ORIENTED_EDGE('',*,*,#4973,.T.);
#6592=ORIENTED_EDGE('',*,*,#4994,.T.);
#6593=ORIENTED_EDGE('',*,*,#4995,.F.);
#6594=ORIENTED_EDGE('',*,*,#4996,.F.);
#6595=ORIENTED_EDGE('',*,*,#4997,.F.);
#6596=ORIENTED_EDGE('',*,*,#4998,.F.);
#6597=ORIENTED_EDGE('',*,*,#4999,.F.);
#6598=ORIENTED_EDGE('',*,*,#5000,.T.);
#6599=ORIENTED_EDGE('',*,*,#5001,.F.);
#6600=ORIENTED_EDGE('',*,*,#5002,.F.);
#6601=ORIENTED_EDGE('',*,*,#5003,.F.);
#6602=ORIENTED_EDGE('',*,*,#5004,.F.);
#6603=ORIENTED_EDGE('',*,*,#5005,.F.);
#6604=ORIENTED_EDGE('',*,*,#5006,.F.);
#6605=ORIENTED_EDGE('',*,*,#5007,.F.);
#6606=ORIENTED_EDGE('',*,*,#5006,.T.);
#6607=ORIENTED_EDGE('',*,*,#5008,.T.);
#6608=ORIENTED_EDGE('',*,*,#4992,.T.);
#6609=ORIENTED_EDGE('',*,*,#5009,.T.);
#6610=ORIENTED_EDGE('',*,*,#5010,.F.);
#6611=ORIENTED_EDGE('',*,*,#5011,.F.);
#6612=ORIENTED_EDGE('',*,*,#5012,.F.);
#6613=ORIENTED_EDGE('',*,*,#5013,.F.);
#6614=ORIENTED_EDGE('',*,*,#5014,.F.);
#6615=ORIENTED_EDGE('',*,*,#5015,.F.);
#6616=ORIENTED_EDGE('',*,*,#5016,.F.);
#6617=ORIENTED_EDGE('',*,*,#5017,.F.);
#6618=ORIENTED_EDGE('',*,*,#5018,.F.);
#6619=ORIENTED_EDGE('',*,*,#5019,.F.);
#6620=ORIENTED_EDGE('',*,*,#5020,.F.);
#6621=ORIENTED_EDGE('',*,*,#5021,.T.);
#6622=ORIENTED_EDGE('',*,*,#5022,.F.);
#6623=ORIENTED_EDGE('',*,*,#5020,.T.);
#6624=ORIENTED_EDGE('',*,*,#5023,.T.);
#6625=ORIENTED_EDGE('',*,*,#5007,.T.);
#6626=ORIENTED_EDGE('',*,*,#5024,.T.);
#6627=ORIENTED_EDGE('',*,*,#5022,.T.);
#6628=ORIENTED_EDGE('',*,*,#5025,.T.);
#6629=ORIENTED_EDGE('',*,*,#5012,.T.);
#6630=ORIENTED_EDGE('',*,*,#5026,.T.);
#6631=ORIENTED_EDGE('',*,*,#5027,.F.);
#6632=ORIENTED_EDGE('',*,*,#5028,.F.);
#6633=ORIENTED_EDGE('',*,*,#5029,.T.);
#6634=ORIENTED_EDGE('',*,*,#5030,.F.);
#6635=ORIENTED_EDGE('',*,*,#5017,.T.);
#6636=ORIENTED_EDGE('',*,*,#5031,.T.);
#6637=ORIENTED_EDGE('',*,*,#5028,.T.);
#6638=ORIENTED_EDGE('',*,*,#5032,.T.);
#6639=ORIENTED_EDGE('',*,*,#5014,.T.);
#6640=ORIENTED_EDGE('',*,*,#5033,.T.);
#6641=ORIENTED_EDGE('',*,*,#5030,.T.);
#6642=ORIENTED_EDGE('',*,*,#5034,.T.);
#6643=ORIENTED_EDGE('',*,*,#5019,.T.);
#6644=ORIENTED_EDGE('',*,*,#5035,.T.);
#6645=ORIENTED_EDGE('',*,*,#5027,.T.);
#6646=ORIENTED_EDGE('',*,*,#5036,.T.);
#6647=ORIENTED_EDGE('',*,*,#5011,.T.);
#6648=ORIENTED_EDGE('',*,*,#5037,.T.);
#6649=ORIENTED_EDGE('',*,*,#5018,.T.);
#6650=ORIENTED_EDGE('',*,*,#5038,.T.);
#6651=ORIENTED_EDGE('',*,*,#5003,.T.);
#6652=ORIENTED_EDGE('',*,*,#5039,.T.);
#6653=ORIENTED_EDGE('',*,*,#5016,.T.);
#6654=ORIENTED_EDGE('',*,*,#5040,.T.);
#6655=ORIENTED_EDGE('',*,*,#4999,.T.);
#6656=ORIENTED_EDGE('',*,*,#5041,.T.);
#6657=ORIENTED_EDGE('',*,*,#5015,.T.);
#6658=ORIENTED_EDGE('',*,*,#5042,.T.);
#6659=ORIENTED_EDGE('',*,*,#5013,.T.);
#6660=ORIENTED_EDGE('',*,*,#5043,.T.);
#6661=ORIENTED_EDGE('',*,*,#5005,.T.);
#6662=ORIENTED_EDGE('',*,*,#5044,.T.);
#6663=ORIENTED_EDGE('',*,*,#4996,.T.);
#6664=ORIENTED_EDGE('',*,*,#5045,.T.);
#6665=ORIENTED_EDGE('',*,*,#5010,.T.);
#6666=ORIENTED_EDGE('',*,*,#5046,.T.);
#6667=ORIENTED_EDGE('',*,*,#4995,.T.);
#6668=ORIENTED_EDGE('',*,*,#5047,.T.);
#6669=ORIENTED_EDGE('',*,*,#5004,.T.);
#6670=ORIENTED_EDGE('',*,*,#5048,.T.);
#6671=ORIENTED_EDGE('',*,*,#5002,.T.);
#6672=ORIENTED_EDGE('',*,*,#5049,.T.);
#6673=ORIENTED_EDGE('',*,*,#4986,.T.);
#6674=ORIENTED_EDGE('',*,*,#5050,.T.);
#6675=ORIENTED_EDGE('',*,*,#4982,.T.);
#6676=ORIENTED_EDGE('',*,*,#5051,.T.);
#6677=ORIENTED_EDGE('',*,*,#5001,.T.);
#6678=ORIENTED_EDGE('',*,*,#5052,.T.);
#6679=ORIENTED_EDGE('',*,*,#4998,.T.);
#6680=ORIENTED_EDGE('',*,*,#5053,.T.);
#6681=ORIENTED_EDGE('',*,*,#4989,.T.);
#6682=ORIENTED_EDGE('',*,*,#5054,.T.);
#6683=ORIENTED_EDGE('',*,*,#4976,.T.);
#6684=ORIENTED_EDGE('',*,*,#5055,.T.);
#6685=ORIENTED_EDGE('',*,*,#4997,.T.);
#6686=ORIENTED_EDGE('',*,*,#5056,.T.);
#6687=ORIENTED_EDGE('',*,*,#4984,.T.);
#6688=ORIENTED_EDGE('',*,*,#5057,.T.);
#6689=ORIENTED_EDGE('',*,*,#4978,.T.);
#6690=ORIENTED_EDGE('',*,*,#5058,.T.);
#6691=ORIENTED_EDGE('',*,*,#4964,.T.);
#6692=ORIENTED_EDGE('',*,*,#5059,.T.);
#6693=ORIENTED_EDGE('',*,*,#4983,.T.);
#6694=ORIENTED_EDGE('',*,*,#5060,.T.);
#6695=ORIENTED_EDGE('',*,*,#4981,.T.);
#6696=ORIENTED_EDGE('',*,*,#5061,.T.);
#6697=ORIENTED_EDGE('',*,*,#4971,.T.);
#6698=ORIENTED_EDGE('',*,*,#5062,.T.);
#6699=ORIENTED_EDGE('',*,*,#4966,.T.);
#6700=ORIENTED_EDGE('',*,*,#5063,.T.);
#6701=ORIENTED_EDGE('',*,*,#4960,.T.);
#6702=ORIENTED_EDGE('',*,*,#5064,.T.);
#6703=ORIENTED_EDGE('',*,*,#4944,.T.);
#6704=ORIENTED_EDGE('',*,*,#5065,.T.);
#6705=ORIENTED_EDGE('',*,*,#4965,.T.);
#6706=ORIENTED_EDGE('',*,*,#5066,.T.);
#6707=ORIENTED_EDGE('',*,*,#4963,.T.);
#6708=ORIENTED_EDGE('',*,*,#5067,.T.);
#6709=ORIENTED_EDGE('',*,*,#4953,.T.);
#6710=ORIENTED_EDGE('',*,*,#5068,.T.);
#6711=ORIENTED_EDGE('',*,*,#4949,.T.);
#6712=ORIENTED_EDGE('',*,*,#5069,.T.);
#6713=ORIENTED_EDGE('',*,*,#4941,.T.);
#6714=ORIENTED_EDGE('',*,*,#5070,.T.);
#6715=ORIENTED_EDGE('',*,*,#4930,.T.);
#6716=ORIENTED_EDGE('',*,*,#5071,.T.);
#6717=ORIENTED_EDGE('',*,*,#4946,.T.);
#6718=ORIENTED_EDGE('',*,*,#5072,.T.);
#6719=ORIENTED_EDGE('',*,*,#4943,.T.);
#6720=ORIENTED_EDGE('',*,*,#5073,.T.);
#6721=ORIENTED_EDGE('',*,*,#4933,.T.);
#6722=ORIENTED_EDGE('',*,*,#5074,.T.);
#6723=ORIENTED_EDGE('',*,*,#4928,.T.);
#6724=ORIENTED_EDGE('',*,*,#5075,.T.);
#6725=ORIENTED_EDGE('',*,*,#4940,.T.);
#6726=ORIENTED_EDGE('',*,*,#5076,.T.);
#6727=ORIENTED_EDGE('',*,*,#4932,.T.);
#6728=ORIENTED_EDGE('',*,*,#5077,.T.);
#6729=ORIENTED_EDGE('',*,*,#4927,.T.);
#6730=ORIENTED_EDGE('',*,*,#5078,.T.);
#6731=ORIENTED_EDGE('',*,*,#4947,.F.);
#6732=ORIENTED_EDGE('',*,*,#4952,.F.);
#6733=ORIENTED_EDGE('',*,*,#5072,.F.);
#6734=ORIENTED_EDGE('',*,*,#4945,.F.);
#6735=ORIENTED_EDGE('',*,*,#5066,.F.);
#6736=ORIENTED_EDGE('',*,*,#5060,.F.);
#6737=ORIENTED_EDGE('',*,*,#5052,.F.);
#6738=ORIENTED_EDGE('',*,*,#5000,.F.);
#6739=ORIENTED_EDGE('',*,*,#5042,.F.);
#6740=ORIENTED_EDGE('',*,*,#5034,.F.);
#6741=ORIENTED_EDGE('',*,*,#5029,.F.);
#6742=ORIENTED_EDGE('',*,*,#5031,.F.);
#6743=ORIENTED_EDGE('',*,*,#5039,.F.);
#6744=ORIENTED_EDGE('',*,*,#5050,.F.);
#6745=ORIENTED_EDGE('',*,*,#4988,.F.);
#6746=ORIENTED_EDGE('',*,*,#4969,.F.);
#6747=ORIENTED_EDGE('',*,*,#4951,.F.);
#6748=ORIENTED_EDGE('',*,*,#5070,.F.);
#6749=ORIENTED_EDGE('',*,*,#5075,.F.);
#6750=ORIENTED_EDGE('',*,*,#5077,.F.);
#6751=ORIENTED_EDGE('',*,*,#4970,.F.);
#6752=ORIENTED_EDGE('',*,*,#5064,.F.);
#6753=ORIENTED_EDGE('',*,*,#4962,.F.);
#6754=ORIENTED_EDGE('',*,*,#5069,.F.);
#6755=ORIENTED_EDGE('',*,*,#4917,.T.);
#6756=ORIENTED_EDGE('',*,*,#4926,.T.);
#6757=ORIENTED_EDGE('',*,*,#4987,.F.);
#6758=ORIENTED_EDGE('',*,*,#5058,.F.);
#6759=ORIENTED_EDGE('',*,*,#4980,.F.);
#6760=ORIENTED_EDGE('',*,*,#5063,.F.);
#6761=ORIENTED_EDGE('',*,*,#5032,.F.);
#6762=ORIENTED_EDGE('',*,*,#5035,.F.);
#6763=ORIENTED_EDGE('',*,*,#5026,.F.);
#6764=ORIENTED_EDGE('',*,*,#5038,.F.);
#6765=ORIENTED_EDGE('',*,*,#5033,.F.);
#6766=ORIENTED_EDGE('',*,*,#5044,.F.);
#6767=ORIENTED_EDGE('',*,*,#5023,.F.);
#6768=ORIENTED_EDGE('',*,*,#5036,.F.);
#6769=ORIENTED_EDGE('',*,*,#5037,.F.);
#6770=ORIENTED_EDGE('',*,*,#5045,.F.);
#6771=ORIENTED_EDGE('',*,*,#5048,.F.);
#6772=ORIENTED_EDGE('',*,*,#5040,.F.);
#6773=ORIENTED_EDGE('',*,*,#5041,.F.);
#6774=ORIENTED_EDGE('',*,*,#5054,.F.);
#6775=ORIENTED_EDGE('',*,*,#5008,.F.);
#6776=ORIENTED_EDGE('',*,*,#5043,.F.);
#6777=ORIENTED_EDGE('',*,*,#5047,.F.);
#6778=ORIENTED_EDGE('',*,*,#5055,.F.);
#6779=ORIENTED_EDGE('',*,*,#5057,.F.);
#6780=ORIENTED_EDGE('',*,*,#5049,.F.);
#6781=ORIENTED_EDGE('',*,*,#4915,.T.);
#6782=ORIENTED_EDGE('',*,*,#4918,.T.);
#6783=ORIENTED_EDGE('',*,*,#4921,.T.);
#6784=ORIENTED_EDGE('',*,*,#4924,.T.);
#6785=ORIENTED_EDGE('',*,*,#5051,.F.);
#6786=ORIENTED_EDGE('',*,*,#5062,.F.);
#6787=ORIENTED_EDGE('',*,*,#4993,.F.);
#6788=ORIENTED_EDGE('',*,*,#5053,.F.);
#6789=ORIENTED_EDGE('',*,*,#5059,.F.);
#6790=ORIENTED_EDGE('',*,*,#5068,.F.);
#6791=ORIENTED_EDGE('',*,*,#4974,.F.);
#6792=ORIENTED_EDGE('',*,*,#5061,.F.);
#6793=ORIENTED_EDGE('',*,*,#5065,.F.);
#6794=ORIENTED_EDGE('',*,*,#5074,.F.);
#6795=ORIENTED_EDGE('',*,*,#4956,.F.);
#6796=ORIENTED_EDGE('',*,*,#5067,.F.);
#6797=ORIENTED_EDGE('',*,*,#5071,.F.);
#6798=ORIENTED_EDGE('',*,*,#5078,.F.);
#6799=ORIENTED_EDGE('',*,*,#4937,.F.);
#6800=ORIENTED_EDGE('',*,*,#5073,.F.);
#6801=ORIENTED_EDGE('',*,*,#4939,.F.);
#6802=ORIENTED_EDGE('',*,*,#4961,.F.);
#6803=ORIENTED_EDGE('',*,*,#4979,.F.);
#6804=ORIENTED_EDGE('',*,*,#5056,.F.);
#6805=ORIENTED_EDGE('',*,*,#5046,.F.);
#6806=ORIENTED_EDGE('',*,*,#5025,.F.);
#6807=ORIENTED_EDGE('',*,*,#5021,.F.);
#6808=ORIENTED_EDGE('',*,*,#5024,.F.);
#6809=ORIENTED_EDGE('',*,*,#5009,.F.);
#6810=ORIENTED_EDGE('',*,*,#4991,.F.);
#6811=ORIENTED_EDGE('',*,*,#4994,.F.);
#6812=ORIENTED_EDGE('',*,*,#4975,.F.);
#6813=ORIENTED_EDGE('',*,*,#4957,.F.);
#6814=ORIENTED_EDGE('',*,*,#4935,.F.);
#6815=ORIENTED_EDGE('',*,*,#4938,.F.);
#6816=ORIENTED_EDGE('',*,*,#5076,.F.);
#8890=PLANE('',#9939);
#8891=PLANE('',#9943);
#8892=PLANE('',#10087);
#8893=PLANE('',#10088);
#8894=PLANE('',#10089);
#8895=PLANE('',#10090);
#8896=PLANE('',#10091);
#8897=PLANE('',#10092);
#8898=PLANE('',#10093);
#8899=PLANE('',#10094);
#8900=PLANE('',#10095);
#8901=PLANE('',#10096);
#8902=PLANE('',#10097);
#8903=PLANE('',#10098);
#8904=PLANE('',#10099);
#8905=PLANE('',#10100);
#9104=ADVANCED_FACE('',(#2117),#368,.F.);
#9105=ADVANCED_FACE('',(#2118),#369,.F.);
#9106=ADVANCED_FACE('',(#2119),#8890,.T.);
#9107=ADVANCED_FACE('',(#2120),#370,.F.);
#9108=ADVANCED_FACE('',(#2121),#8891,.T.);
#9109=ADVANCED_FACE('',(#2122),#371,.F.);
#9110=ADVANCED_FACE('',(#2123),#133,.T.);
#9111=ADVANCED_FACE('',(#2124),#134,.T.);
#9112=ADVANCED_FACE('',(#2125),#219,.T.);
#9113=ADVANCED_FACE('',(#2126),#372,.T.);
#9114=ADVANCED_FACE('',(#2127),#220,.T.);
#9115=ADVANCED_FACE('',(#2128),#221,.T.);
#9116=ADVANCED_FACE('',(#2129),#222,.T.);
#9117=ADVANCED_FACE('',(#2130),#373,.T.);
#9118=ADVANCED_FACE('',(#2131),#135,.T.);
#9119=ADVANCED_FACE('',(#2132),#374,.T.);
#9120=ADVANCED_FACE('',(#2133),#136,.T.);
#9121=ADVANCED_FACE('',(#2134),#375,.T.);
#9122=ADVANCED_FACE('',(#2135),#137,.T.);
#9123=ADVANCED_FACE('',(#2136),#138,.T.);
#9124=ADVANCED_FACE('',(#2137),#376,.T.);
#9125=ADVANCED_FACE('',(#2138),#139,.T.);
#9126=ADVANCED_FACE('',(#2139),#377,.T.);
#9127=ADVANCED_FACE('',(#2140),#140,.T.);
#9128=ADVANCED_FACE('',(#2141),#378,.T.);
#9129=ADVANCED_FACE('',(#2142),#141,.T.);
#9130=ADVANCED_FACE('',(#2143),#142,.T.);
#9131=ADVANCED_FACE('',(#2144),#379,.T.);
#9132=ADVANCED_FACE('',(#2145),#223,.T.);
#9133=ADVANCED_FACE('',(#2146),#380,.T.);
#9134=ADVANCED_FACE('',(#2147),#143,.T.);
#9135=ADVANCED_FACE('',(#2148),#224,.T.);
#9136=ADVANCED_FACE('',(#2149),#144,.T.);
#9137=ADVANCED_FACE('',(#2150),#145,.T.);
#9138=ADVANCED_FACE('',(#2151),#381,.T.);
#9139=ADVANCED_FACE('',(#2152),#146,.T.);
#9140=ADVANCED_FACE('',(#2153),#147,.T.);
#9141=ADVANCED_FACE('',(#2154),#148,.T.);
#9142=ADVANCED_FACE('',(#2155),#225,.T.);
#9143=ADVANCED_FACE('',(#2156),#382,.T.);
#9144=ADVANCED_FACE('',(#2157),#383,.T.);
#9145=ADVANCED_FACE('',(#2158),#226,.T.);
#9146=ADVANCED_FACE('',(#2159),#384,.T.);
#9147=ADVANCED_FACE('',(#2160),#385,.T.);
#9148=ADVANCED_FACE('',(#2161),#386,.F.);
#9149=ADVANCED_FACE('',(#2162),#387,.T.);
#9150=ADVANCED_FACE('',(#2163),#388,.T.);
#9151=ADVANCED_FACE('',(#2164),#389,.T.);
#9152=ADVANCED_FACE('',(#2165),#390,.T.);
#9153=ADVANCED_FACE('',(#2166),#391,.T.);
#9154=ADVANCED_FACE('',(#2167),#392,.T.);
#9155=ADVANCED_FACE('',(#2168),#393,.T.);
#9156=ADVANCED_FACE('',(#2169),#394,.T.);
#9157=ADVANCED_FACE('',(#2170),#395,.F.);
#9158=ADVANCED_FACE('',(#2171),#396,.T.);
#9159=ADVANCED_FACE('',(#2172),#397,.T.);
#9160=ADVANCED_FACE('',(#2173),#398,.T.);
#9161=ADVANCED_FACE('',(#2174),#399,.T.);
#9162=ADVANCED_FACE('',(#2175),#400,.T.);
#9163=ADVANCED_FACE('',(#2176),#401,.T.);
#9164=ADVANCED_FACE('',(#2177),#402,.T.);
#9165=ADVANCED_FACE('',(#2178),#403,.F.);
#9166=ADVANCED_FACE('',(#2179),#404,.T.);
#9167=ADVANCED_FACE('',(#2180),#405,.F.);
#9168=ADVANCED_FACE('',(#2181),#406,.T.);
#9169=ADVANCED_FACE('',(#2182),#407,.T.);
#9170=ADVANCED_FACE('',(#2183),#8892,.T.);
#9171=ADVANCED_FACE('',(#2184),#8893,.T.);
#9172=ADVANCED_FACE('',(#2185,#1975,#1976),#8894,.F.);
#9173=ADVANCED_FACE('',(#2186),#8895,.T.);
#9174=ADVANCED_FACE('',(#2187),#8896,.F.);
#9175=ADVANCED_FACE('',(#2188),#8897,.T.);
#9176=ADVANCED_FACE('',(#2189),#8898,.T.);
#9177=ADVANCED_FACE('',(#2190),#8899,.T.);
#9178=ADVANCED_FACE('',(#2191,#1977,#1978,#1979,#1980),#8900,.T.);
#9179=ADVANCED_FACE('',(#2192),#8901,.T.);
#9180=ADVANCED_FACE('',(#2193),#8902,.T.);
#9181=ADVANCED_FACE('',(#2194),#8903,.T.);
#9182=ADVANCED_FACE('',(#2195),#8904,.T.);
#9183=ADVANCED_FACE('',(#2196),#8905,.T.);
#9630=CLOSED_SHELL('',(#9104,#9105,#9106,#9107,#9108,#9109,#9110,#9111,
#9112,#9113,#9114,#9115,#9116,#9117,#9118,#9119,#9120,#9121,#9122,#9123,
#9124,#9125,#9126,#9127,#9128,#9129,#9130,#9131,#9132,#9133,#9134,#9135,
#9136,#9137,#9138,#9139,#9140,#9141,#9142,#9143,#9144,#9145,#9146,#9147,
#9148,#9149,#9150,#9151,#9152,#9153,#9154,#9155,#9156,#9157,#9158,#9159,
#9160,#9161,#9162,#9163,#9164,#9165,#9166,#9167,#9168,#9169,#9170,#9171,
#9172,#9173,#9174,#9175,#9176,#9177,#9178,#9179,#9180,#9181,#9182,#9183));
#9932=AXIS2_PLACEMENT_3D('',#14657,#11501,#11502);
#9933=AXIS2_PLACEMENT_3D('',#14658,#11503,#11504);
#9934=AXIS2_PLACEMENT_3D('',#14660,#11505,#11506);
#9935=AXIS2_PLACEMENT_3D('',#14663,#11508,#11509);
#9936=AXIS2_PLACEMENT_3D('',#14664,#11510,#11511);
#9937=AXIS2_PLACEMENT_3D('',#14666,#11512,#11513);
#9938=AXIS2_PLACEMENT_3D('',#14669,#11515,#11516);
#9939=AXIS2_PLACEMENT_3D('',#14670,#11517,#11518);
#9940=AXIS2_PLACEMENT_3D('',#14671,#11519,#11520);
#9941=AXIS2_PLACEMENT_3D('',#14673,#11521,#11522);
#9942=AXIS2_PLACEMENT_3D('',#14676,#11524,#11525);
#9943=AXIS2_PLACEMENT_3D('',#14677,#11526,#11527);
#9944=AXIS2_PLACEMENT_3D('',#14678,#11528,#11529);
#9945=AXIS2_PLACEMENT_3D('',#14680,#11530,#11531);
#9946=AXIS2_PLACEMENT_3D('',#14683,#11533,#11534);
#9947=AXIS2_PLACEMENT_3D('',#14684,#11535,#11536);
#9948=AXIS2_PLACEMENT_3D('',#14687,#11537,#11538);
#9949=AXIS2_PLACEMENT_3D('',#14689,#11539,#11540);
#9950=AXIS2_PLACEMENT_3D('',#14690,#11541,#11542);
#9951=AXIS2_PLACEMENT_3D('',#14691,#11543,#11544);
#9952=AXIS2_PLACEMENT_3D('',#14694,#11545,#11546);
#9953=AXIS2_PLACEMENT_3D('',#14696,#11547,#11548);
#9954=AXIS2_PLACEMENT_3D('',#14697,#11549,#11550);
#9955=AXIS2_PLACEMENT_3D('',#14698,#11551,#11552);
#9956=AXIS2_PLACEMENT_3D('',#14701,#11553,#11554);
#9957=AXIS2_PLACEMENT_3D('',#14703,#11555,#11556);
#9958=AXIS2_PLACEMENT_3D('',#14705,#11557,#11558);
#9959=AXIS2_PLACEMENT_3D('',#14706,#11559,#11560);
#9960=AXIS2_PLACEMENT_3D('',#14707,#11561,#11562);
#9961=AXIS2_PLACEMENT_3D('',#14710,#11565,#11566);
#9962=AXIS2_PLACEMENT_3D('',#14713,#11567,#11568);
#9963=AXIS2_PLACEMENT_3D('',#14715,#11569,#11570);
#9964=AXIS2_PLACEMENT_3D('',#14717,#11571,#11572);
#9965=AXIS2_PLACEMENT_3D('',#14718,#11573,#11574);
#9966=AXIS2_PLACEMENT_3D('',#14719,#11575,#11576);
#9967=AXIS2_PLACEMENT_3D('',#14722,#11577,#11578);
#9968=AXIS2_PLACEMENT_3D('',#14724,#11579,#11580);
#9969=AXIS2_PLACEMENT_3D('',#14726,#11581,#11582);
#9970=AXIS2_PLACEMENT_3D('',#14727,#11583,#11584);
#9971=AXIS2_PLACEMENT_3D('',#14728,#11585,#11586);
#9972=AXIS2_PLACEMENT_3D('',#14731,#11587,#11588);
#9973=AXIS2_PLACEMENT_3D('',#14733,#11589,#11590);
#9974=AXIS2_PLACEMENT_3D('',#14735,#11591,#11592);
#9975=AXIS2_PLACEMENT_3D('',#14736,#11593,#11594);
#9976=AXIS2_PLACEMENT_3D('',#14737,#11595,#11596);
#9977=AXIS2_PLACEMENT_3D('',#14740,#11599,#11600);
#9978=AXIS2_PLACEMENT_3D('',#14743,#11601,#11602);
#9979=AXIS2_PLACEMENT_3D('',#14745,#11603,#11604);
#9980=AXIS2_PLACEMENT_3D('',#14746,#11605,#11606);
#9981=AXIS2_PLACEMENT_3D('',#14747,#11607,#11608);
#9982=AXIS2_PLACEMENT_3D('',#14750,#11611,#11612);
#9983=AXIS2_PLACEMENT_3D('',#14753,#11613,#11614);
#9984=AXIS2_PLACEMENT_3D('',#14755,#11615,#11616);
#9985=AXIS2_PLACEMENT_3D('',#14756,#11617,#11618);
#9986=AXIS2_PLACEMENT_3D('',#14757,#11619,#11620);
#9987=AXIS2_PLACEMENT_3D('',#14760,#11623,#11624);
#9988=AXIS2_PLACEMENT_3D('',#14763,#11625,#11626);
#9989=AXIS2_PLACEMENT_3D('',#14765,#11627,#11628);
#9990=AXIS2_PLACEMENT_3D('',#14766,#11629,#11630);
#9991=AXIS2_PLACEMENT_3D('',#14767,#11631,#11632);
#9992=AXIS2_PLACEMENT_3D('',#14770,#11633,#11634);
#9993=AXIS2_PLACEMENT_3D('',#14772,#11635,#11636);
#9994=AXIS2_PLACEMENT_3D('',#14773,#11637,#11638);
#9995=AXIS2_PLACEMENT_3D('',#14774,#11639,#11640);
#9996=AXIS2_PLACEMENT_3D('',#14777,#11643,#11644);
#9997=AXIS2_PLACEMENT_3D('',#14780,#11645,#11646);
#9998=AXIS2_PLACEMENT_3D('',#14782,#11647,#11648);
#9999=AXIS2_PLACEMENT_3D('',#14783,#11649,#11650);
#10000=AXIS2_PLACEMENT_3D('',#14784,#11651,#11652);
#10001=AXIS2_PLACEMENT_3D('',#14787,#11655,#11656);
#10002=AXIS2_PLACEMENT_3D('',#14790,#11657,#11658);
#10003=AXIS2_PLACEMENT_3D('',#14792,#11659,#11660);
#10004=AXIS2_PLACEMENT_3D('',#14793,#11661,#11662);
#10005=AXIS2_PLACEMENT_3D('',#14794,#11663,#11664);
#10006=AXIS2_PLACEMENT_3D('',#14797,#11667,#11668);
#10007=AXIS2_PLACEMENT_3D('',#14800,#11669,#11670);
#10008=AXIS2_PLACEMENT_3D('',#14802,#11671,#11672);
#10009=AXIS2_PLACEMENT_3D('',#14803,#11673,#11674);
#10010=AXIS2_PLACEMENT_3D('',#14804,#11675,#11676);
#10011=AXIS2_PLACEMENT_3D('',#14807,#11677,#11678);
#10012=AXIS2_PLACEMENT_3D('',#14809,#11679,#11680);
#10013=AXIS2_PLACEMENT_3D('',#14810,#11681,#11682);
#10014=AXIS2_PLACEMENT_3D('',#14811,#11683,#11684);
#10015=AXIS2_PLACEMENT_3D('',#14814,#11687,#11688);
#10016=AXIS2_PLACEMENT_3D('',#14817,#11689,#11690);
#10017=AXIS2_PLACEMENT_3D('',#14819,#11691,#11692);
#10018=AXIS2_PLACEMENT_3D('',#14821,#11693,#11694);
#10019=AXIS2_PLACEMENT_3D('',#14822,#11695,#11696);
#10020=AXIS2_PLACEMENT_3D('',#14823,#11697,#11698);
#10021=AXIS2_PLACEMENT_3D('',#14826,#11701,#11702);
#10022=AXIS2_PLACEMENT_3D('',#14829,#11703,#11704);
#10023=AXIS2_PLACEMENT_3D('',#14831,#11705,#11706);
#10024=AXIS2_PLACEMENT_3D('',#14832,#11707,#11708);
#10025=AXIS2_PLACEMENT_3D('',#14833,#11709,#11710);
#10026=AXIS2_PLACEMENT_3D('',#14836,#11711,#11712);
#10027=AXIS2_PLACEMENT_3D('',#14838,#11713,#11714);
#10028=AXIS2_PLACEMENT_3D('',#14840,#11715,#11716);
#10029=AXIS2_PLACEMENT_3D('',#14841,#11717,#11718);
#10030=AXIS2_PLACEMENT_3D('',#14842,#11719,#11720);
#10031=AXIS2_PLACEMENT_3D('',#14845,#11721,#11722);
#10032=AXIS2_PLACEMENT_3D('',#14847,#11723,#11724);
#10033=AXIS2_PLACEMENT_3D('',#14848,#11725,#11726);
#10034=AXIS2_PLACEMENT_3D('',#14849,#11727,#11728);
#10035=AXIS2_PLACEMENT_3D('',#14852,#11729,#11730);
#10036=AXIS2_PLACEMENT_3D('',#14854,#11731,#11732);
#10037=AXIS2_PLACEMENT_3D('',#14855,#11733,#11734);
#10038=AXIS2_PLACEMENT_3D('',#14856,#11735,#11736);
#10039=AXIS2_PLACEMENT_3D('',#14859,#11739,#11740);
#10040=AXIS2_PLACEMENT_3D('',#14862,#11741,#11742);
#10041=AXIS2_PLACEMENT_3D('',#14864,#11743,#11744);
#10042=AXIS2_PLACEMENT_3D('',#14865,#11745,#11746);
#10043=AXIS2_PLACEMENT_3D('',#14866,#11747,#11748);
#10044=AXIS2_PLACEMENT_3D('',#14869,#11749,#11750);
#10045=AXIS2_PLACEMENT_3D('',#14871,#11751,#11752);
#10046=AXIS2_PLACEMENT_3D('',#14872,#11753,#11754);
#10047=AXIS2_PLACEMENT_3D('',#14873,#11755,#11756);
#10048=AXIS2_PLACEMENT_3D('',#14876,#11757,#11758);
#10049=AXIS2_PLACEMENT_3D('',#14878,#11759,#11760);
#10050=AXIS2_PLACEMENT_3D('',#14879,#11761,#11762);
#10051=AXIS2_PLACEMENT_3D('',#14880,#11763,#11764);
#10052=AXIS2_PLACEMENT_3D('',#14883,#11765,#11766);
#10053=AXIS2_PLACEMENT_3D('',#14885,#11767,#11768);
#10054=AXIS2_PLACEMENT_3D('',#14887,#11769,#11770);
#10055=AXIS2_PLACEMENT_3D('',#14888,#11771,#11772);
#10056=AXIS2_PLACEMENT_3D('',#14889,#11773,#11774);
#10057=AXIS2_PLACEMENT_3D('',#14892,#11777,#11778);
#10058=AXIS2_PLACEMENT_3D('',#14895,#11781,#11782);
#10059=AXIS2_PLACEMENT_3D('',#14898,#11783,#11784);
#10060=AXIS2_PLACEMENT_3D('',#14900,#11785,#11786);
#10061=AXIS2_PLACEMENT_3D('',#14902,#11787,#11788);
#10062=AXIS2_PLACEMENT_3D('',#14903,#11789,#11790);
#10063=AXIS2_PLACEMENT_3D('',#14904,#11791,#11792);
#10064=AXIS2_PLACEMENT_3D('',#14907,#11795,#11796);
#10065=AXIS2_PLACEMENT_3D('',#14910,#11799,#11800);
#10066=AXIS2_PLACEMENT_3D('',#14913,#11803,#11804);
#10067=AXIS2_PLACEMENT_3D('',#14916,#11807,#11808);
#10068=AXIS2_PLACEMENT_3D('',#14919,#11811,#11812);
#10069=AXIS2_PLACEMENT_3D('',#14922,#11815,#11816);
#10070=AXIS2_PLACEMENT_3D('',#14925,#11819,#11820);
#10071=AXIS2_PLACEMENT_3D('',#14928,#11823,#11824);
#10072=AXIS2_PLACEMENT_3D('',#14931,#11827,#11828);
#10073=AXIS2_PLACEMENT_3D('',#14934,#11831,#11832);
#10074=AXIS2_PLACEMENT_3D('',#14937,#11835,#11836);
#10075=AXIS2_PLACEMENT_3D('',#14940,#11839,#11840);
#10076=AXIS2_PLACEMENT_3D('',#14943,#11843,#11844);
#10077=AXIS2_PLACEMENT_3D('',#14946,#11847,#11848);
#10078=AXIS2_PLACEMENT_3D('',#14949,#11851,#11852);
#10079=AXIS2_PLACEMENT_3D('',#14952,#11855,#11856);
#10080=AXIS2_PLACEMENT_3D('',#14955,#11859,#11860);
#10081=AXIS2_PLACEMENT_3D('',#14958,#11863,#11864);
#10082=AXIS2_PLACEMENT_3D('',#14961,#11867,#11868);
#10083=AXIS2_PLACEMENT_3D('',#14964,#11871,#11872);
#10084=AXIS2_PLACEMENT_3D('',#14967,#11875,#11876);
#10085=AXIS2_PLACEMENT_3D('',#14970,#11879,#11880);
#10086=AXIS2_PLACEMENT_3D('',#14973,#11883,#11884);
#10087=AXIS2_PLACEMENT_3D('',#14976,#11887,#11888);
#10088=AXIS2_PLACEMENT_3D('',#14977,#11889,#11890);
#10089=AXIS2_PLACEMENT_3D('',#14978,#11891,#11892);
#10090=AXIS2_PLACEMENT_3D('',#14979,#11893,#11894);
#10091=AXIS2_PLACEMENT_3D('',#14980,#11895,#11896);
#10092=AXIS2_PLACEMENT_3D('',#14981,#11897,#11898);
#10093=AXIS2_PLACEMENT_3D('',#14982,#11899,#11900);
#10094=AXIS2_PLACEMENT_3D('',#14983,#11901,#11902);
#10095=AXIS2_PLACEMENT_3D('',#14984,#11903,#11904);
#10096=AXIS2_PLACEMENT_3D('',#14985,#11905,#11906);
#10097=AXIS2_PLACEMENT_3D('',#14986,#11907,#11908);
#10098=AXIS2_PLACEMENT_3D('',#14987,#11909,#11910);
#10099=AXIS2_PLACEMENT_3D('',#14988,#11911,#11912);
#10100=AXIS2_PLACEMENT_3D('',#14989,#11913,#11914);
#11501=DIRECTION('axis',(0.,0.,1.));
#11502=DIRECTION('refdir',(1.,0.,0.));
#11503=DIRECTION('center_axis',(0.,0.,-1.));
#11504=DIRECTION('ref_axis',(-1.,0.,0.));
#11505=DIRECTION('center_axis',(0.,0.,-1.));
#11506=DIRECTION('ref_axis',(-1.,0.,0.));
#11507=DIRECTION('',(0.,0.,-1.));
#11508=DIRECTION('center_axis',(0.,0.,1.));
#11509=DIRECTION('ref_axis',(-1.,0.,0.));
#11510=DIRECTION('center_axis',(0.,0.,-1.));
#11511=DIRECTION('ref_axis',(-1.,0.,0.));
#11512=DIRECTION('center_axis',(0.,0.,-1.));
#11513=DIRECTION('ref_axis',(-1.,0.,0.));
#11514=DIRECTION('',(0.,0.,-1.));
#11515=DIRECTION('center_axis',(0.,0.,-1.));
#11516=DIRECTION('ref_axis',(-1.,0.,0.));
#11517=DIRECTION('center_axis',(0.,0.,1.));
#11518=DIRECTION('ref_axis',(-1.,0.,0.));
#11519=DIRECTION('center_axis',(0.,0.,-1.));
#11520=DIRECTION('ref_axis',(-1.,0.,0.));
#11521=DIRECTION('center_axis',(0.,0.,-1.));
#11522=DIRECTION('ref_axis',(-1.,0.,0.));
#11523=DIRECTION('',(0.,0.,-1.));
#11524=DIRECTION('center_axis',(0.,0.,-1.));
#11525=DIRECTION('ref_axis',(-1.,0.,0.));
#11526=DIRECTION('center_axis',(0.,0.,1.));
#11527=DIRECTION('ref_axis',(-1.,0.,0.));
#11528=DIRECTION('center_axis',(0.,0.,-1.));
#11529=DIRECTION('ref_axis',(-1.,0.,0.));
#11530=DIRECTION('center_axis',(0.,0.,-1.));
#11531=DIRECTION('ref_axis',(-1.,0.,0.));
#11532=DIRECTION('',(0.,0.,-1.));
#11533=DIRECTION('center_axis',(0.,0.,1.));
#11534=DIRECTION('ref_axis',(-1.,0.,0.));
#11535=DIRECTION('center_axis',(-0.827465426020391,-0.538877990790891,0.15783370927044));
#11536=DIRECTION('ref_axis',(-0.561516668266297,0.79410448776086,-0.232587819494442));
#11537=DIRECTION('center_axis',(7.105427357601E-14,1.,7.105427357601E-14));
#11538=DIRECTION('ref_axis',(-0.707106781186548,0.,0.707106781186548));
#11539=DIRECTION('center_axis',(-0.707106781186552,0.,-0.707106781186543));
#11540=DIRECTION('ref_axis',(0.,1.,0.));
#11541=DIRECTION('center_axis',(-1.,0.,0.));
#11542=DIRECTION('ref_axis',(0.,0.,-1.));
#11543=DIRECTION('center_axis',(-0.827465426020364,0.53887799079092,0.157833709270477));
#11544=DIRECTION('ref_axis',(-0.561516668266353,-0.794104487760813,-0.232587819494468));
#11545=DIRECTION('center_axis',(-1.,0.,0.));
#11546=DIRECTION('ref_axis',(0.,-1.,0.));
#11547=DIRECTION('center_axis',(-0.707106781186548,0.,-0.707106781186548));
#11548=DIRECTION('ref_axis',(-0.707106781186548,0.,0.707106781186548));
#11549=DIRECTION('center_axis',(0.,-1.,0.));
#11550=DIRECTION('ref_axis',(0.,0.,-1.));
#11551=DIRECTION('center_axis',(0.,-1.,0.));
#11552=DIRECTION('ref_axis',(0.,0.,-1.));
#11553=DIRECTION('center_axis',(0.,-1.,0.));
#11554=DIRECTION('ref_axis',(0.,0.,1.));
#11555=DIRECTION('center_axis',(-1.,0.,0.));
#11556=DIRECTION('ref_axis',(0.,1.,0.));
#11557=DIRECTION('center_axis',(0.,1.,0.));
#11558=DIRECTION('ref_axis',(0.707106781186549,0.,0.707106781186546));
#11559=DIRECTION('center_axis',(0.,0.,-1.));
#11560=DIRECTION('ref_axis',(-1.,0.,0.));
#11561=DIRECTION('center_axis',(1.,0.,0.));
#11562=DIRECTION('ref_axis',(0.,0.707106781186554,-0.707106781186541));
#11563=DIRECTION('',(-1.,0.,0.));
#11564=DIRECTION('',(1.,0.,0.));
#11565=DIRECTION('center_axis',(0.,-1.,3.5527136788003E-14));
#11566=DIRECTION('ref_axis',(0.,-2.84217094304039E-14,-1.));
#11567=DIRECTION('center_axis',(0.,1.,0.));
#11568=DIRECTION('ref_axis',(0.923879532511286,0.,0.382683432365093));
#11569=DIRECTION('center_axis',(-0.707106781186543,-2.51214793389392E-14,
-0.707106781186552));
#11570=DIRECTION('ref_axis',(-0.707106781186552,0.,0.707106781186543));
#11571=DIRECTION('center_axis',(-5.02429586778809E-14,-1.,0.));
#11572=DIRECTION('ref_axis',(0.,0.,1.));
#11573=DIRECTION('center_axis',(-1.,0.,0.));
#11574=DIRECTION('ref_axis',(0.,1.,0.));
#11575=DIRECTION('center_axis',(0.,1.,0.));
#11576=DIRECTION('ref_axis',(0.,0.,1.));
#11577=DIRECTION('center_axis',(0.,1.,0.));
#11578=DIRECTION('ref_axis',(1.,0.,0.));
#11579=DIRECTION('center_axis',(0.,0.,-1.));
#11580=DIRECTION('ref_axis',(0.,-1.,0.));
#11581=DIRECTION('center_axis',(0.,-1.,0.));
#11582=DIRECTION('ref_axis',(0.707106781186549,0.,0.707106781186546));
#11583=DIRECTION('center_axis',(-1.,0.,0.));
#11584=DIRECTION('ref_axis',(0.,0.,-1.));
#11585=DIRECTION('center_axis',(0.,1.,0.));
#11586=DIRECTION('ref_axis',(0.,0.,1.));
#11587=DIRECTION('center_axis',(0.,-1.,0.));
#11588=DIRECTION('ref_axis',(0.9238795325113,0.,0.382683432365059));
#11589=DIRECTION('center_axis',(-1.,0.,0.));
#11590=DIRECTION('ref_axis',(0.,0.,-1.));
#11591=DIRECTION('center_axis',(0.,1.,0.));
#11592=DIRECTION('ref_axis',(0.707106781186548,0.,-0.707106781186548));
#11593=DIRECTION('center_axis',(-0.707106781186539,0.,-0.707106781186556));
#11594=DIRECTION('ref_axis',(0.,-1.,0.));
#11595=DIRECTION('center_axis',(0.707106781186548,0.,0.707106781186548));
#11596=DIRECTION('ref_axis',(-0.499999999999994,-0.707106781186551,0.500000000000001));
#11597=DIRECTION('',(-0.707106781186548,0.,-0.707106781186548));
#11598=DIRECTION('',(0.707106781186548,0.,0.707106781186548));
#11599=DIRECTION('center_axis',(-0.816496580927733,-0.408248290463856,0.408248290463857));
#11600=DIRECTION('ref_axis',(-0.577350269189618,0.57735026918964,-0.577350269189619));
#11601=DIRECTION('center_axis',(0.,1.,0.));
#11602=DIRECTION('ref_axis',(-1.,0.,0.));
#11603=DIRECTION('center_axis',(0.,0.,-1.));
#11604=DIRECTION('ref_axis',(0.,1.,0.));
#11605=DIRECTION('center_axis',(-1.,0.,0.));
#11606=DIRECTION('ref_axis',(0.,0.,-1.));
#11607=DIRECTION('center_axis',(0.,0.,-1.));
#11608=DIRECTION('ref_axis',(-0.707106781186541,0.707106781186554,0.));
#11609=DIRECTION('',(0.,0.,1.));
#11610=DIRECTION('',(0.,0.,-1.));
#11611=DIRECTION('center_axis',(0.408248290463858,-0.408248290463858,-0.816496580927731));
#11612=DIRECTION('ref_axis',(-0.577350269189628,0.577350269189628,-0.577350269189621));
#11613=DIRECTION('center_axis',(0.,0.,-1.));
#11614=DIRECTION('ref_axis',(0.,1.,0.));
#11615=DIRECTION('center_axis',(-1.,0.,0.));
#11616=DIRECTION('ref_axis',(0.,0.,-1.));
#11617=DIRECTION('center_axis',(0.,1.,0.));
#11618=DIRECTION('ref_axis',(-1.,0.,0.));
#11619=DIRECTION('center_axis',(-1.,0.,0.));
#11620=DIRECTION('ref_axis',(0.,0.707106781186554,-0.707106781186541));
#11621=DIRECTION('',(1.,0.,0.));
#11622=DIRECTION('',(-1.,0.,0.));
#11623=DIRECTION('center_axis',(-0.816496580927731,0.408248290463855,0.40824829046386));
#11624=DIRECTION('ref_axis',(-0.577350269189618,-0.577350269189639,-0.57735026918962));
#11625=DIRECTION('center_axis',(0.,-1.,0.));
#11626=DIRECTION('ref_axis',(0.,0.,-1.));
#11627=DIRECTION('center_axis',(-1.,0.,0.));
#11628=DIRECTION('ref_axis',(0.,-1.,0.));
#11629=DIRECTION('center_axis',(0.,0.,-1.));
#11630=DIRECTION('ref_axis',(-1.,0.,0.));
#11631=DIRECTION('center_axis',(0.408248290463854,0.408248290463854,-0.816496580927736));
#11632=DIRECTION('ref_axis',(-0.577350269189645,-0.577350269189616,-0.577350269189616));
#11633=DIRECTION('center_axis',(0.,-1.,0.));
#11634=DIRECTION('ref_axis',(0.,0.,-1.));
#11635=DIRECTION('center_axis',(-1.,0.,1.77635683940026E-14));
#11636=DIRECTION('ref_axis',(0.,-1.,0.));
#11637=DIRECTION('center_axis',(0.,0.,-1.));
#11638=DIRECTION('ref_axis',(-1.,0.,0.));
#11639=DIRECTION('center_axis',(1.,0.,0.));
#11640=DIRECTION('ref_axis',(0.,-0.707106781186554,-0.707106781186541));
#11641=DIRECTION('',(-1.,0.,0.));
#11642=DIRECTION('',(1.,0.,0.));
#11643=DIRECTION('center_axis',(-0.816496580927732,0.408248290463855,-0.408248290463859));
#11644=DIRECTION('ref_axis',(0.577350269189618,0.57735026918964,-0.577350269189619));
#11645=DIRECTION('center_axis',(0.,1.,0.));
#11646=DIRECTION('ref_axis',(0.,0.,-1.));
#11647=DIRECTION('center_axis',(1.,0.,0.));
#11648=DIRECTION('ref_axis',(0.,1.,0.));
#11649=DIRECTION('center_axis',(0.,-2.22044604925028E-15,-1.));
#11650=DIRECTION('ref_axis',(1.,0.,0.));
#11651=DIRECTION('center_axis',(1.,0.,0.));
#11652=DIRECTION('ref_axis',(0.,0.707106781186553,-0.707106781186542));
#11653=DIRECTION('',(-1.,0.,0.));
#11654=DIRECTION('',(1.,0.,0.));
#11655=DIRECTION('center_axis',(-0.816496580927724,-0.408248290463876,-0.408248290463855));
#11656=DIRECTION('ref_axis',(-0.577350269189633,0.577350269189633,0.577350269189612));
#11657=DIRECTION('center_axis',(-1.,0.,0.));
#11658=DIRECTION('ref_axis',(0.,1.,0.));
#11659=DIRECTION('center_axis',(0.,0.,1.));
#11660=DIRECTION('ref_axis',(-1.,0.,0.));
#11661=DIRECTION('center_axis',(0.,1.,0.));
#11662=DIRECTION('ref_axis',(0.,0.,1.));
#11663=DIRECTION('center_axis',(0.,0.,1.));
#11664=DIRECTION('ref_axis',(-0.707106781186548,0.707106781186548,0.));
#11665=DIRECTION('',(0.,0.,-1.));
#11666=DIRECTION('',(0.,0.,1.));
#11667=DIRECTION('center_axis',(-0.816496580927732,-0.408248290463855,-0.408248290463859));
#11668=DIRECTION('ref_axis',(0.577350269189618,-0.57735026918964,-0.577350269189619));
#11669=DIRECTION('center_axis',(0.,-1.,0.));
#11670=DIRECTION('ref_axis',(1.,0.,0.));
#11671=DIRECTION('center_axis',(2.22044604925032E-15,0.,-1.));
#11672=DIRECTION('ref_axis',(0.,-1.,0.));
#11673=DIRECTION('center_axis',(1.,0.,0.));
#11674=DIRECTION('ref_axis',(0.,0.,-1.));
#11675=DIRECTION('center_axis',(-0.408248290463854,-0.408248290463854,-0.816496580927736));
#11676=DIRECTION('ref_axis',(-0.577350269189645,-0.577350269189616,0.577350269189616));
#11677=DIRECTION('center_axis',(0.,-1.,0.));
#11678=DIRECTION('ref_axis',(-1.,0.,0.));
#11679=DIRECTION('center_axis',(0.,0.,1.));
#11680=DIRECTION('ref_axis',(0.,-1.,0.));
#11681=DIRECTION('center_axis',(-1.,-1.77635683940023E-14,0.));
#11682=DIRECTION('ref_axis',(0.,0.,1.));
#11683=DIRECTION('center_axis',(0.,0.,1.));
#11684=DIRECTION('ref_axis',(-0.707106781186548,-0.707106781186548,0.));
#11685=DIRECTION('',(0.,0.,-1.));
#11686=DIRECTION('',(0.,0.,1.));
#11687=DIRECTION('center_axis',(0.,-1.,0.));
#11688=DIRECTION('ref_axis',(0.,0.,-1.));
#11689=DIRECTION('center_axis',(0.,-1.,0.));
#11690=DIRECTION('ref_axis',(-1.,0.,0.));
#11691=DIRECTION('center_axis',(0.,0.,-1.));
#11692=DIRECTION('ref_axis',(0.,1.,0.));
#11693=DIRECTION('center_axis',(0.,1.,0.));
#11694=DIRECTION('ref_axis',(-0.707106781186546,0.,0.707106781186549));
#11695=DIRECTION('center_axis',(1.,0.,0.));
#11696=DIRECTION('ref_axis',(0.,0.,-1.));
#11697=DIRECTION('center_axis',(0.,0.,1.));
#11698=DIRECTION('ref_axis',(0.707106781186541,0.707106781186554,0.));
#11699=DIRECTION('',(0.,0.,-1.));
#11700=DIRECTION('',(0.,0.,1.));
#11701=DIRECTION('center_axis',(0.408248290463854,0.408248290463854,-0.816496580927736));
#11702=DIRECTION('ref_axis',(0.577350269189645,0.577350269189616,0.577350269189616));
#11703=DIRECTION('center_axis',(0.,1.,0.));
#11704=DIRECTION('ref_axis',(1.,0.,0.));
#11705=DIRECTION('center_axis',(0.,0.,1.));
#11706=DIRECTION('ref_axis',(0.,1.,0.));
#11707=DIRECTION('center_axis',(1.,1.77635683940023E-14,0.));
#11708=DIRECTION('ref_axis',(0.,0.,1.));
#11709=DIRECTION('center_axis',(0.,1.,0.));
#11710=DIRECTION('ref_axis',(0.,0.,1.));
#11711=DIRECTION('center_axis',(0.,1.,0.));
#11712=DIRECTION('ref_axis',(0.,0.,1.));
#11713=DIRECTION('center_axis',(1.,0.,0.));
#11714=DIRECTION('ref_axis',(0.,-1.,0.));
#11715=DIRECTION('center_axis',(0.,-1.,0.));
#11716=DIRECTION('ref_axis',(-0.707106781186549,0.,0.707106781186546));
#11717=DIRECTION('center_axis',(0.,0.,-1.));
#11718=DIRECTION('ref_axis',(1.,0.,0.));
#11719=DIRECTION('center_axis',(-0.816496580927724,-0.408248290463876,0.408248290463855));
#11720=DIRECTION('ref_axis',(0.577350269189633,-0.577350269189633,0.577350269189612));
#11721=DIRECTION('center_axis',(1.,0.,0.));
#11722=DIRECTION('ref_axis',(0.,-1.,0.));
#11723=DIRECTION('center_axis',(0.,0.,1.));
#11724=DIRECTION('ref_axis',(1.,0.,0.));
#11725=DIRECTION('center_axis',(0.,-1.,0.));
#11726=DIRECTION('ref_axis',(0.,0.,1.));
#11727=DIRECTION('center_axis',(-0.408248290463855,-0.408248290463855,-0.816496580927734));
#11728=DIRECTION('ref_axis',(0.577350269189645,0.577350269189616,-0.577350269189616));
#11729=DIRECTION('center_axis',(0.,1.,0.));
#11730=DIRECTION('ref_axis',(0.,0.,-1.));
#11731=DIRECTION('center_axis',(1.,0.,1.77635683940026E-14));
#11732=DIRECTION('ref_axis',(0.,1.,0.));
#11733=DIRECTION('center_axis',(0.,0.,-1.));
#11734=DIRECTION('ref_axis',(1.,0.,0.));
#11735=DIRECTION('center_axis',(1.,0.,0.));
#11736=DIRECTION('ref_axis',(0.,0.707106781186554,-0.707106781186541));
#11737=DIRECTION('',(-1.,0.,0.));
#11738=DIRECTION('',(1.,0.,0.));
#11739=DIRECTION('center_axis',(-0.816496580927728,0.408248290463864,-0.408248290463857));
#11740=DIRECTION('ref_axis',(0.577350269189626,0.577350269189626,-0.577350269189626));
#11741=DIRECTION('center_axis',(0.,0.,-1.));
#11742=DIRECTION('ref_axis',(1.,0.,0.));
#11743=DIRECTION('center_axis',(0.,1.,0.));
#11744=DIRECTION('ref_axis',(0.,0.,-1.));
#11745=DIRECTION('center_axis',(1.,0.,1.77635683940026E-14));
#11746=DIRECTION('ref_axis',(0.,1.,0.));
#11747=DIRECTION('center_axis',(-0.408248290463855,0.408248290463855,-0.816496580927734));
#11748=DIRECTION('ref_axis',(0.577350269189645,-0.577350269189616,-0.577350269189616));
#11749=DIRECTION('center_axis',(0.,-1.,0.));
#11750=DIRECTION('ref_axis',(1.,0.,0.));
#11751=DIRECTION('center_axis',(0.,0.,-1.));
#11752=DIRECTION('ref_axis',(0.,-1.,0.));
#11753=DIRECTION('center_axis',(1.,0.,0.));
#11754=DIRECTION('ref_axis',(0.,0.,-1.));
#11755=DIRECTION('center_axis',(-0.408248290463858,0.408248290463858,-0.816496580927731));
#11756=DIRECTION('ref_axis',(0.577350269189628,-0.577350269189628,-0.577350269189621));
#11757=DIRECTION('center_axis',(0.,0.,-1.));
#11758=DIRECTION('ref_axis',(0.,-1.,0.));
#11759=DIRECTION('center_axis',(1.,0.,0.));
#11760=DIRECTION('ref_axis',(0.,0.,-1.));
#11761=DIRECTION('center_axis',(0.,-1.,0.));
#11762=DIRECTION('ref_axis',(1.,0.,0.));
#11763=DIRECTION('center_axis',(0.,-1.,0.));
#11764=DIRECTION('ref_axis',(0.,0.,-1.));
#11765=DIRECTION('center_axis',(0.,-1.,0.));
#11766=DIRECTION('ref_axis',(-1.,0.,0.));
#11767=DIRECTION('center_axis',(0.,0.,-1.));
#11768=DIRECTION('ref_axis',(0.,1.,0.));
#11769=DIRECTION('center_axis',(0.,1.,0.));
#11770=DIRECTION('ref_axis',(-0.707106781186548,0.,0.707106781186548));
#11771=DIRECTION('center_axis',(1.,0.,0.));
#11772=DIRECTION('ref_axis',(0.,0.,-1.));
#11773=DIRECTION('center_axis',(0.,0.,1.));
#11774=DIRECTION('ref_axis',(0.707106781186548,0.707106781186548,0.));
#11775=DIRECTION('',(0.,0.,-1.));
#11776=DIRECTION('',(0.,0.,1.));
#11777=DIRECTION('center_axis',(-1.,0.,0.));
#11778=DIRECTION('ref_axis',(0.,0.707106781186554,-0.707106781186541));
#11779=DIRECTION('',(1.,0.,0.));
#11780=DIRECTION('',(-1.,0.,0.));
#11781=DIRECTION('center_axis',(0.,1.,0.));
#11782=DIRECTION('ref_axis',(0.,0.,1.));
#11783=DIRECTION('center_axis',(0.,1.,0.));
#11784=DIRECTION('ref_axis',(0.,0.,1.));
#11785=DIRECTION('center_axis',(1.,0.,0.));
#11786=DIRECTION('ref_axis',(0.,-1.,0.));
#11787=DIRECTION('center_axis',(0.,-1.,0.));
#11788=DIRECTION('ref_axis',(-0.707106781186548,0.,0.707106781186548));
#11789=DIRECTION('center_axis',(0.,0.,-1.));
#11790=DIRECTION('ref_axis',(1.,0.,0.));
#11791=DIRECTION('center_axis',(1.,0.,0.));
#11792=DIRECTION('ref_axis',(0.,-0.707106781186554,-0.707106781186541));
#11793=DIRECTION('',(-1.,0.,0.));
#11794=DIRECTION('',(1.,0.,0.));
#11795=DIRECTION('center_axis',(0.,0.,-1.));
#11796=DIRECTION('ref_axis',(0.707106781186548,-0.707106781186548,0.));
#11797=DIRECTION('',(0.,0.,1.));
#11798=DIRECTION('',(0.,0.,-1.));
#11799=DIRECTION('center_axis',(0.,1.,0.));
#11800=DIRECTION('ref_axis',(-0.707106781186541,0.,0.707106781186554));
#11801=DIRECTION('',(0.,-1.,0.));
#11802=DIRECTION('',(0.,1.,0.));
#11803=DIRECTION('center_axis',(0.,1.,0.));
#11804=DIRECTION('ref_axis',(0.707106781186541,0.,-0.707106781186554));
#11805=DIRECTION('',(0.,-1.,0.));
#11806=DIRECTION('',(0.,1.,0.));
#11807=DIRECTION('center_axis',(0.,0.,1.));
#11808=DIRECTION('ref_axis',(0.707106781186548,-0.707106781186548,0.));
#11809=DIRECTION('',(0.,0.,-1.));
#11810=DIRECTION('',(0.,0.,1.));
#11811=DIRECTION('center_axis',(-1.,0.,0.));
#11812=DIRECTION('ref_axis',(0.,-0.707106781186554,-0.707106781186541));
#11813=DIRECTION('',(1.,0.,0.));
#11814=DIRECTION('',(-1.,0.,0.));
#11815=DIRECTION('center_axis',(0.,-1.,0.));
#11816=DIRECTION('ref_axis',(0.707106781186541,0.,-0.707106781186554));
#11817=DIRECTION('',(0.,1.,0.));
#11818=DIRECTION('',(0.,-1.,0.));
#11819=DIRECTION('center_axis',(0.,0.,1.));
#11820=DIRECTION('ref_axis',(0.707106781186548,0.707106781186548,0.));
#11821=DIRECTION('',(0.,0.,-1.));
#11822=DIRECTION('',(0.,0.,1.));
#11823=DIRECTION('center_axis',(0.,1.,0.));
#11824=DIRECTION('ref_axis',(0.707106781186541,0.,0.707106781186554));
#11825=DIRECTION('',(0.,-1.,0.));
#11826=DIRECTION('',(0.,1.,0.));
#11827=DIRECTION('center_axis',(1.,0.,0.));
#11828=DIRECTION('ref_axis',(0.,-0.707106781186554,0.707106781186541));
#11829=DIRECTION('',(-1.,0.,0.));
#11830=DIRECTION('',(1.,0.,0.));
#11831=DIRECTION('center_axis',(0.,0.,-1.));
#11832=DIRECTION('ref_axis',(0.707106781186541,-0.707106781186554,0.));
#11833=DIRECTION('',(0.,0.,1.));
#11834=DIRECTION('',(0.,0.,-1.));
#11835=DIRECTION('center_axis',(0.,-1.,0.));
#11836=DIRECTION('ref_axis',(-0.707106781186544,0.,0.707106781186551));
#11837=DIRECTION('',(0.,1.,0.));
#11838=DIRECTION('',(0.,-1.,0.));
#11839=DIRECTION('center_axis',(-1.,0.,0.));
#11840=DIRECTION('ref_axis',(0.,0.707106781186554,0.707106781186541));
#11841=DIRECTION('',(1.,0.,0.));
#11842=DIRECTION('',(-1.,0.,0.));
#11843=DIRECTION('center_axis',(0.,-1.,0.));
#11844=DIRECTION('ref_axis',(-0.707106781186541,0.,0.707106781186554));
#11845=DIRECTION('',(0.,1.,0.));
#11846=DIRECTION('',(0.,-1.,0.));
#11847=DIRECTION('center_axis',(-1.,0.,0.));
#11848=DIRECTION('ref_axis',(0.,-0.707106781186553,-0.707106781186542));
#11849=DIRECTION('',(1.,0.,0.));
#11850=DIRECTION('',(-1.,0.,0.));
#11851=DIRECTION('center_axis',(0.,-1.,0.));
#11852=DIRECTION('ref_axis',(0.707106781186546,0.,-0.707106781186549));
#11853=DIRECTION('',(0.,1.,0.));
#11854=DIRECTION('',(0.,-1.,0.));
#11855=DIRECTION('center_axis',(0.,-1.,0.));
#11856=DIRECTION('ref_axis',(-0.707106781186541,0.,-0.707106781186554));
#11857=DIRECTION('',(0.,1.,0.));
#11858=DIRECTION('',(0.,-1.,0.));
#11859=DIRECTION('center_axis',(0.,0.,1.));
#11860=DIRECTION('ref_axis',(-0.707106781186541,-0.707106781186554,0.));
#11861=DIRECTION('',(0.,0.,-1.));
#11862=DIRECTION('',(0.,0.,1.));
#11863=DIRECTION('center_axis',(0.,-1.,0.));
#11864=DIRECTION('ref_axis',(-0.707106781186547,0.,-0.707106781186548));
#11865=DIRECTION('',(0.,1.,0.));
#11866=DIRECTION('',(0.,-1.,0.));
#11867=DIRECTION('center_axis',(0.,-1.,0.));
#11868=DIRECTION('ref_axis',(0.923879532511288,0.,0.382683432365088));
#11869=DIRECTION('',(0.,1.,0.));
#11870=DIRECTION('',(0.,-1.,0.));
#11871=DIRECTION('center_axis',(-1.,0.,0.));
#11872=DIRECTION('ref_axis',(0.,-0.707106781186554,-0.707106781186541));
#11873=DIRECTION('',(1.,0.,0.));
#11874=DIRECTION('',(-1.,0.,0.));
#11875=DIRECTION('center_axis',(0.,-1.,0.));
#11876=DIRECTION('ref_axis',(0.707106781186548,0.,0.707106781186548));
#11877=DIRECTION('',(0.,1.,0.));
#11878=DIRECTION('',(0.,-1.,0.));
#11879=DIRECTION('center_axis',(-0.707106781186548,0.,-0.707106781186548));
#11880=DIRECTION('ref_axis',(-0.499999999999997,0.707106781186553,0.499999999999996));
#11881=DIRECTION('',(0.707106781186548,0.,0.707106781186548));
#11882=DIRECTION('',(-0.707106781186548,0.,-0.707106781186548));
#11883=DIRECTION('center_axis',(0.,-1.,0.));
#11884=DIRECTION('ref_axis',(-0.923879532511283,0.,-0.382683432365098));
#11885=DIRECTION('',(0.,1.,0.));
#11886=DIRECTION('',(0.,-1.,0.));
#11887=DIRECTION('center_axis',(0.,-1.,0.));
#11888=DIRECTION('ref_axis',(1.,0.,0.));
#11889=DIRECTION('center_axis',(-0.707106781186548,0.,0.707106781186548));
#11890=DIRECTION('ref_axis',(-0.707106781186548,0.,-0.707106781186548));
#11891=DIRECTION('center_axis',(0.,0.,1.));
#11892=DIRECTION('ref_axis',(-1.,0.,0.));
#11893=DIRECTION('center_axis',(-1.,0.,0.));
#11894=DIRECTION('ref_axis',(0.,-1.,0.));
#11895=DIRECTION('center_axis',(0.,0.,1.));
#11896=DIRECTION('ref_axis',(-1.,0.,0.));
#11897=DIRECTION('center_axis',(1.,0.,0.));
#11898=DIRECTION('ref_axis',(0.,0.,1.));
#11899=DIRECTION('center_axis',(1.,0.,0.));
#11900=DIRECTION('ref_axis',(0.,1.,0.));
#11901=DIRECTION('center_axis',(0.,0.,-1.));
#11902=DIRECTION('ref_axis',(1.,0.,0.));
#11903=DIRECTION('center_axis',(0.,0.,1.));
#11904=DIRECTION('ref_axis',(1.,0.,0.));
#11905=DIRECTION('center_axis',(1.,0.,0.));
#11906=DIRECTION('ref_axis',(0.,0.,1.));
#11907=DIRECTION('center_axis',(0.,0.,-1.));
#11908=DIRECTION('ref_axis',(1.,0.,0.));
#11909=DIRECTION('center_axis',(-1.,0.,0.));
#11910=DIRECTION('ref_axis',(0.,0.,-1.));
#11911=DIRECTION('center_axis',(0.,0.,-1.));
#11912=DIRECTION('ref_axis',(1.,0.,0.));
#11913=DIRECTION('center_axis',(0.,1.,0.));
#11914=DIRECTION('ref_axis',(-1.,0.,0.));
#14657=CARTESIAN_POINT('',(0.,0.,0.));
#14658=CARTESIAN_POINT('Origin',(-29.5614402453126,-77.3500535736325,32.));
#14659=CARTESIAN_POINT('',(-23.5614402453126,-77.3500535736325,32.));
#14660=CARTESIAN_POINT('Origin',(-29.5614402453126,-77.3500535736325,32.));
#14661=CARTESIAN_POINT('',(-23.5614402453126,-77.3500535736325,20.));
#14662=CARTESIAN_POINT('',(-23.5614402453126,-77.3500535736325,32.));
#14663=CARTESIAN_POINT('Origin',(-29.5614402453126,-77.3500535736325,20.));
#14664=CARTESIAN_POINT('Origin',(29.5614402453126,77.3500535736325,32.));
#14665=CARTESIAN_POINT('',(35.5614402453126,77.3500535736325,32.));
#14666=CARTESIAN_POINT('Origin',(29.5614402453126,77.3500535736325,32.));
#14667=CARTESIAN_POINT('',(35.5614402453126,77.3500535736325,20.));
#14668=CARTESIAN_POINT('',(35.5614402453126,77.3500535736325,32.));
#14669=CARTESIAN_POINT('Origin',(29.5614402453126,77.3500535736325,20.));
#14670=CARTESIAN_POINT('Origin',(29.5614402453126,77.3500535736325,20.));
#14671=CARTESIAN_POINT('Origin',(29.5614402453126,-77.3500535736325,32.));
#14672=CARTESIAN_POINT('',(35.5614402453126,-77.3500535736325,32.));
#14673=CARTESIAN_POINT('Origin',(29.5614402453126,-77.3500535736325,32.));
#14674=CARTESIAN_POINT('',(35.5614402453126,-77.3500535736325,20.));
#14675=CARTESIAN_POINT('',(35.5614402453126,-77.3500535736325,32.));
#14676=CARTESIAN_POINT('Origin',(29.5614402453126,-77.3500535736325,20.));
#14677=CARTESIAN_POINT('Origin',(29.5614402453126,-77.3500535736325,20.));
#14678=CARTESIAN_POINT('Origin',(-29.5614402453126,77.3500535736325,32.));
#14679=CARTESIAN_POINT('',(-23.5614402453126,77.3500535736325,32.));
#14680=CARTESIAN_POINT('Origin',(-29.5614402453126,77.3500535736325,32.));
#14681=CARTESIAN_POINT('',(-23.5614402453126,77.3500535736325,20.));
#14682=CARTESIAN_POINT('',(-23.5614402453126,77.3500535736325,32.));
#14683=CARTESIAN_POINT('Origin',(-29.5614402453126,77.3500535736325,20.));
#14684=CARTESIAN_POINT('Origin',(-24.92755355845,89.5,16.1978257430375));
#14685=CARTESIAN_POINT('',(-25.2811069490433,89.5,16.5513791336308));
#14686=CARTESIAN_POINT('',(-24.92755355845,89.5,15.6978257430375));
#14687=CARTESIAN_POINT('Origin',(-24.92755355845,89.5,16.1978257430375));
#14688=CARTESIAN_POINT('',(-24.92755355845,90.,16.1978257430375));
#14689=CARTESIAN_POINT('Origin',(-24.92755355845,89.5,16.1978257430375));
#14690=CARTESIAN_POINT('Origin',(-24.92755355845,89.5,16.1978257430375));
#14691=CARTESIAN_POINT('Origin',(-24.92755355845,-89.5,16.1978257430375));
#14692=CARTESIAN_POINT('',(-24.92755355845,-90.,16.1978257430375));
#14693=CARTESIAN_POINT('',(-24.92755355845,-89.5,15.6978257430375));
#14694=CARTESIAN_POINT('Origin',(-24.92755355845,-89.5,16.1978257430375));
#14695=CARTESIAN_POINT('',(-25.2811069490433,-89.5,16.5513791336308));
#14696=CARTESIAN_POINT('Origin',(-24.92755355845,-89.5,16.1978257430375));
#14697=CARTESIAN_POINT('Origin',(-24.92755355845,-89.5,16.1978257430375));
#14698=CARTESIAN_POINT('Origin',(-19.545300072509,89.5,15.1978257430375));
#14699=CARTESIAN_POINT('',(-19.545300072509,89.5,15.6978257430375));
#14700=CARTESIAN_POINT('',(-19.045300072509,89.5,15.1978257430375));
#14701=CARTESIAN_POINT('Origin',(-19.545300072509,89.5,15.1978257430375));
#14702=CARTESIAN_POINT('',(-19.545300072509,90.,16.1978257430375));
#14703=CARTESIAN_POINT('Origin',(-19.545300072509,89.5,16.1978257430375));
#14704=CARTESIAN_POINT('',(-18.545300072509,90.,15.1978257430375));
#14705=CARTESIAN_POINT('Origin',(-19.545300072509,90.,15.1978257430375));
#14706=CARTESIAN_POINT('Origin',(-18.545300072509,89.5,15.1978257430375));
#14707=CARTESIAN_POINT('Origin',(19.4326698301817,89.5,16.1978257430375));
#14708=CARTESIAN_POINT('',(19.4326698301817,89.5,15.6978257430375));
#14709=CARTESIAN_POINT('',(19.4326698301817,90.,16.1978257430375));
#14710=CARTESIAN_POINT('Origin',(-23.0395928638606,89.5,19.5));
#14711=CARTESIAN_POINT('',(-23.0395928638606,90.,20.5));
#14712=CARTESIAN_POINT('',(-22.3324860826741,90.,18.7928932188135));
#14713=CARTESIAN_POINT('Origin',(-23.0395928638606,90.,19.5));
#14714=CARTESIAN_POINT('',(-22.6860394732673,89.5,19.1464466094067));
#14715=CARTESIAN_POINT('Origin',(-22.3324860826741,89.5,18.7928932188135));
#14716=CARTESIAN_POINT('',(-23.0395928638606,89.5,20.));
#14717=CARTESIAN_POINT('Origin',(-23.0395928638606,89.5,19.5));
#14718=CARTESIAN_POINT('Origin',(-23.0395928638606,89.5,20.5));
#14719=CARTESIAN_POINT('Origin',(-19.545300072509,-89.5,15.1978257430375));
#14720=CARTESIAN_POINT('',(-19.045300072509,-89.5,15.1978257430375));
#14721=CARTESIAN_POINT('',(-19.545300072509,-89.5,15.6978257430375));
#14722=CARTESIAN_POINT('Origin',(-19.545300072509,-89.5,15.1978257430375));
#14723=CARTESIAN_POINT('',(-18.545300072509,-90.,15.1978257430375));
#14724=CARTESIAN_POINT('Origin',(-18.545300072509,-89.5,15.1978257430375));
#14725=CARTESIAN_POINT('',(-19.545300072509,-90.,16.1978257430375));
#14726=CARTESIAN_POINT('Origin',(-19.545300072509,-90.,15.1978257430375));
#14727=CARTESIAN_POINT('Origin',(-19.545300072509,-89.5,16.1978257430375));
#14728=CARTESIAN_POINT('Origin',(-23.0395928638606,-89.5,19.5));
#14729=CARTESIAN_POINT('',(-22.3324860826741,-90.,18.7928932188135));
#14730=CARTESIAN_POINT('',(-23.0395928638606,-90.,20.5));
#14731=CARTESIAN_POINT('Origin',(-23.0395928638606,-90.,19.5));
#14732=CARTESIAN_POINT('',(-23.0395928638606,-89.5,20.));
#14733=CARTESIAN_POINT('Origin',(-23.0395928638606,-89.5,20.5));
#14734=CARTESIAN_POINT('',(-22.6860394732673,-89.5,19.1464466094067));
#14735=CARTESIAN_POINT('Origin',(-23.0395928638606,-89.5,19.5));
#14736=CARTESIAN_POINT('Origin',(-22.3324860826741,-89.5,18.7928932188135));
#14737=CARTESIAN_POINT('Origin',(-32.2708111714123,-89.5,8.85456813007524));
#14738=CARTESIAN_POINT('',(-32.6243645620056,-89.5,9.20812152066852));
#14739=CARTESIAN_POINT('',(-32.2708111714123,-90.,8.85456813007524));
#14740=CARTESIAN_POINT('Origin',(-18.545300072509,89.5,4.19782574303749));
#14741=CARTESIAN_POINT('',(-19.045300072509,89.5,4.19782574303749));
#14742=CARTESIAN_POINT('',(-18.545300072509,89.5,3.69782574303749));
#14743=CARTESIAN_POINT('Origin',(-18.545300072509,89.5,4.19782574303749));
#14744=CARTESIAN_POINT('',(-18.545300072509,90.,4.19782574303749));
#14745=CARTESIAN_POINT('Origin',(-18.545300072509,89.5,4.19782574303749));
#14746=CARTESIAN_POINT('Origin',(-18.545300072509,89.5,4.19782574303749));
#14747=CARTESIAN_POINT('Origin',(-18.545300072509,89.5,17.8489128715187));
#14748=CARTESIAN_POINT('',(-19.045300072509,89.5,17.8489128715187));
#14749=CARTESIAN_POINT('',(-18.545300072509,90.,17.8489128715187));
#14750=CARTESIAN_POINT('Origin',(-64.5,89.5,20.5));
#14751=CARTESIAN_POINT('',(-64.5,90.,20.5));
#14752=CARTESIAN_POINT('',(-65.,89.5,20.5));
#14753=CARTESIAN_POINT('Origin',(-64.5,89.5,20.5));
#14754=CARTESIAN_POINT('',(-64.5,89.5,20.));
#14755=CARTESIAN_POINT('Origin',(-64.5,89.5,20.5));
#14756=CARTESIAN_POINT('Origin',(-64.5,89.5,20.5));
#14757=CARTESIAN_POINT('Origin',(32.5,89.5,20.5));
#14758=CARTESIAN_POINT('',(32.5,90.,20.5));
#14759=CARTESIAN_POINT('',(32.5,89.5,20.));
#14760=CARTESIAN_POINT('Origin',(-18.545300072509,-89.5,4.19782574303749));
#14761=CARTESIAN_POINT('',(-18.545300072509,-89.5,3.69782574303749));
#14762=CARTESIAN_POINT('',(-19.045300072509,-89.5,4.19782574303749));
#14763=CARTESIAN_POINT('Origin',(-18.545300072509,-89.5,4.19782574303749));
#14764=CARTESIAN_POINT('',(-18.545300072509,-90.,4.19782574303749));
#14765=CARTESIAN_POINT('Origin',(-18.545300072509,-89.5,4.19782574303749));
#14766=CARTESIAN_POINT('Origin',(-18.545300072509,-89.5,4.19782574303749));
#14767=CARTESIAN_POINT('Origin',(-64.5,-89.5,20.5));
#14768=CARTESIAN_POINT('',(-64.5,-89.5,20.));
#14769=CARTESIAN_POINT('',(-65.,-89.5,20.5));
#14770=CARTESIAN_POINT('Origin',(-64.5,-89.5,20.5));
#14771=CARTESIAN_POINT('',(-64.5,-90.,20.5));
#14772=CARTESIAN_POINT('Origin',(-64.5,-89.5,20.5));
#14773=CARTESIAN_POINT('Origin',(-64.5,-89.5,20.5));
#14774=CARTESIAN_POINT('Origin',(-32.5,-89.5,20.5));
#14775=CARTESIAN_POINT('',(-32.5,-90.,20.5));
#14776=CARTESIAN_POINT('',(-32.5,-89.5,20.));
#14777=CARTESIAN_POINT('Origin',(21.0741207385024,89.5,4.19782574303749));
#14778=CARTESIAN_POINT('',(21.0741207385024,89.5,3.69782574303749));
#14779=CARTESIAN_POINT('',(21.5741207385024,89.5,4.19782574303749));
#14780=CARTESIAN_POINT('Origin',(21.0741207385024,89.5,4.19782574303749));
#14781=CARTESIAN_POINT('',(21.0741207385024,90.,4.19782574303749));
#14782=CARTESIAN_POINT('Origin',(21.0741207385024,89.5,4.19782574303749));
#14783=CARTESIAN_POINT('Origin',(21.0741207385024,89.5,4.19782574303749));
#14784=CARTESIAN_POINT('Origin',(22.9773499637455,89.5,4.19782574303749));
#14785=CARTESIAN_POINT('',(22.9773499637455,89.5,3.69782574303749));
#14786=CARTESIAN_POINT('',(22.9773499637455,90.,4.19782574303749));
#14787=CARTESIAN_POINT('Origin',(-64.5,89.5,31.5));
#14788=CARTESIAN_POINT('',(-64.5,90.,31.5));
#14789=CARTESIAN_POINT('',(-64.5,89.5,32.));
#14790=CARTESIAN_POINT('Origin',(-64.5,89.5,31.5));
#14791=CARTESIAN_POINT('',(-65.,89.5,31.5));
#14792=CARTESIAN_POINT('Origin',(-64.5,89.5,31.5));
#14793=CARTESIAN_POINT('Origin',(-64.5,89.5,31.5));
#14794=CARTESIAN_POINT('Origin',(-64.5,89.5,20.));
#14795=CARTESIAN_POINT('',(-64.5,90.,20.));
#14796=CARTESIAN_POINT('',(-65.,89.5,20.));
#14797=CARTESIAN_POINT('Origin',(21.0741207385024,-89.5,4.19782574303749));
#14798=CARTESIAN_POINT('',(21.5741207385024,-89.5,4.19782574303749));
#14799=CARTESIAN_POINT('',(21.0741207385024,-89.5,3.69782574303749));
#14800=CARTESIAN_POINT('Origin',(21.0741207385024,-89.5,4.19782574303749));
#14801=CARTESIAN_POINT('',(21.0741207385024,-90.,4.19782574303749));
#14802=CARTESIAN_POINT('Origin',(21.0741207385024,-89.5,4.19782574303749));
#14803=CARTESIAN_POINT('Origin',(21.0741207385024,-89.5,4.19782574303749));
#14804=CARTESIAN_POINT('Origin',(-64.5,-89.5,31.5));
#14805=CARTESIAN_POINT('',(-65.,-89.5,31.5));
#14806=CARTESIAN_POINT('',(-64.5,-89.5,32.));
#14807=CARTESIAN_POINT('Origin',(-64.5,-89.5,31.5));
#14808=CARTESIAN_POINT('',(-64.5,-90.,31.5));
#14809=CARTESIAN_POINT('Origin',(-64.5,-89.5,31.5));
#14810=CARTESIAN_POINT('Origin',(-64.5,-89.5,31.5));
#14811=CARTESIAN_POINT('Origin',(-64.5,-89.5,20.));
#14812=CARTESIAN_POINT('',(-65.,-89.5,20.));
#14813=CARTESIAN_POINT('',(-64.5,-90.,20.));
#14814=CARTESIAN_POINT('Origin',(22.0741207385024,89.5,15.1978257430375));
#14815=CARTESIAN_POINT('',(21.5741207385024,89.5,15.1978257430375));
#14816=CARTESIAN_POINT('',(22.0741207385024,89.5,15.6978257430375));
#14817=CARTESIAN_POINT('Origin',(22.0741207385024,89.5,15.1978257430375));
#14818=CARTESIAN_POINT('',(21.0741207385024,90.,15.1978257430375));
#14819=CARTESIAN_POINT('Origin',(21.0741207385024,89.5,15.1978257430375));
#14820=CARTESIAN_POINT('',(22.0741207385024,90.,16.1978257430375));
#14821=CARTESIAN_POINT('Origin',(22.0741207385024,90.,15.1978257430375));
#14822=CARTESIAN_POINT('Origin',(22.0741207385024,89.5,16.1978257430375));
#14823=CARTESIAN_POINT('Origin',(21.0741207385024,89.5,11.8489128715187));
#14824=CARTESIAN_POINT('',(21.5741207385024,89.5,11.8489128715187));
#14825=CARTESIAN_POINT('',(21.0741207385024,90.,11.8489128715187));
#14826=CARTESIAN_POINT('Origin',(64.5,89.5,31.5));
#14827=CARTESIAN_POINT('',(65.,89.5,31.5));
#14828=CARTESIAN_POINT('',(64.5,89.5,32.));
#14829=CARTESIAN_POINT('Origin',(64.5,89.5,31.5));
#14830=CARTESIAN_POINT('',(64.5,90.,31.5));
#14831=CARTESIAN_POINT('Origin',(64.5,89.5,31.5));
#14832=CARTESIAN_POINT('Origin',(64.5,89.5,31.5));
#14833=CARTESIAN_POINT('Origin',(22.0741207385024,-89.5,15.1978257430375));
#14834=CARTESIAN_POINT('',(22.0741207385024,-89.5,15.6978257430375));
#14835=CARTESIAN_POINT('',(21.5741207385024,-89.5,15.1978257430375));
#14836=CARTESIAN_POINT('Origin',(22.0741207385024,-89.5,15.1978257430375));
#14837=CARTESIAN_POINT('',(22.0741207385024,-90.,16.1978257430375));
#14838=CARTESIAN_POINT('Origin',(22.0741207385024,-89.5,16.1978257430375));
#14839=CARTESIAN_POINT('',(21.0741207385024,-90.,15.1978257430375));
#14840=CARTESIAN_POINT('Origin',(22.0741207385024,-90.,15.1978257430375));
#14841=CARTESIAN_POINT('Origin',(21.0741207385024,-89.5,15.1978257430375));
#14842=CARTESIAN_POINT('Origin',(64.5,-89.5,31.5));
#14843=CARTESIAN_POINT('',(64.5,-90.,31.5));
#14844=CARTESIAN_POINT('',(64.5,-89.5,32.));
#14845=CARTESIAN_POINT('Origin',(64.5,-89.5,31.5));
#14846=CARTESIAN_POINT('',(65.,-89.5,31.5));
#14847=CARTESIAN_POINT('Origin',(64.5,-89.5,31.5));
#14848=CARTESIAN_POINT('Origin',(64.5,-89.5,31.5));
#14849=CARTESIAN_POINT('Origin',(44.3272645584124,89.5,16.1978257430375));
#14850=CARTESIAN_POINT('',(44.3272645584125,89.5,15.6978257430375));
#14851=CARTESIAN_POINT('',(44.8272645584125,89.5,16.1978257430375));
#14852=CARTESIAN_POINT('Origin',(44.3272645584125,89.5,16.1978257430375));
#14853=CARTESIAN_POINT('',(44.3272645584124,90.,16.1978257430375));
#14854=CARTESIAN_POINT('Origin',(44.3272645584124,89.5,16.1978257430375));
#14855=CARTESIAN_POINT('Origin',(44.3272645584124,89.5,16.1978257430375));
#14856=CARTESIAN_POINT('Origin',(43.2870603692512,89.5,16.1978257430375));
#14857=CARTESIAN_POINT('',(43.2870603692512,89.5,15.6978257430375));
#14858=CARTESIAN_POINT('',(43.2870603692512,90.,16.1978257430375));
#14859=CARTESIAN_POINT('Origin',(64.5,89.5,20.5));
#14860=CARTESIAN_POINT('',(65.,89.5,20.5));
#14861=CARTESIAN_POINT('',(64.5,90.,20.5));
#14862=CARTESIAN_POINT('Origin',(64.5,89.5,20.5));
#14863=CARTESIAN_POINT('',(64.5,89.5,20.));
#14864=CARTESIAN_POINT('Origin',(64.5,89.5,20.5));
#14865=CARTESIAN_POINT('Origin',(64.5,89.5,20.5));
#14866=CARTESIAN_POINT('Origin',(44.3272645584124,-89.5,16.1978257430375));
#14867=CARTESIAN_POINT('',(44.8272645584125,-89.5,16.1978257430375));
#14868=CARTESIAN_POINT('',(44.3272645584125,-89.5,15.6978257430375));
#14869=CARTESIAN_POINT('Origin',(44.3272645584125,-89.5,16.1978257430375));
#14870=CARTESIAN_POINT('',(44.3272645584124,-90.,16.1978257430375));
#14871=CARTESIAN_POINT('Origin',(44.3272645584124,-89.5,16.1978257430375));
#14872=CARTESIAN_POINT('Origin',(44.3272645584124,-89.5,16.1978257430375));
#14873=CARTESIAN_POINT('Origin',(64.5,-89.5,20.5));
#14874=CARTESIAN_POINT('',(64.5,-90.,20.5));
#14875=CARTESIAN_POINT('',(65.,-89.5,20.5));
#14876=CARTESIAN_POINT('Origin',(64.5,-89.5,20.5));
#14877=CARTESIAN_POINT('',(64.5,-89.5,20.));
#14878=CARTESIAN_POINT('Origin',(64.5,-89.5,20.5));
#14879=CARTESIAN_POINT('Origin',(64.5,-89.5,20.5));
#14880=CARTESIAN_POINT('Origin',(45.3272645584125,89.5,19.5));
#14881=CARTESIAN_POINT('',(44.8272645584125,89.5,19.5));
#14882=CARTESIAN_POINT('',(45.3272645584125,89.5,20.));
#14883=CARTESIAN_POINT('Origin',(45.3272645584125,89.5,19.5));
#14884=CARTESIAN_POINT('',(44.3272645584124,90.,19.5));
#14885=CARTESIAN_POINT('Origin',(44.3272645584124,89.5,19.5));
#14886=CARTESIAN_POINT('',(45.3272645584125,90.,20.5));
#14887=CARTESIAN_POINT('Origin',(45.3272645584125,90.,19.5));
#14888=CARTESIAN_POINT('Origin',(45.3272645584125,89.5,20.5));
#14889=CARTESIAN_POINT('Origin',(44.3272645584124,89.5,17.8489128715187));
#14890=CARTESIAN_POINT('',(44.8272645584125,89.5,17.8489128715187));
#14891=CARTESIAN_POINT('',(44.3272645584124,90.,17.8489128715187));
#14892=CARTESIAN_POINT('Origin',(32.5,89.5,20.5));
#14893=CARTESIAN_POINT('',(32.5,90.,20.5));
#14894=CARTESIAN_POINT('',(32.5,89.5,20.));
#14895=CARTESIAN_POINT('Origin',(45.3272645584125,-89.5,19.5));
#14896=CARTESIAN_POINT('',(45.3272645584125,-89.5,20.));
#14897=CARTESIAN_POINT('',(44.8272645584125,-89.5,19.5));
#14898=CARTESIAN_POINT('Origin',(45.3272645584125,-89.5,19.5));
#14899=CARTESIAN_POINT('',(45.3272645584125,-90.,20.5));
#14900=CARTESIAN_POINT('Origin',(45.3272645584125,-89.5,20.5));
#14901=CARTESIAN_POINT('',(44.3272645584124,-90.,19.5));
#14902=CARTESIAN_POINT('Origin',(45.3272645584125,-90.,19.5));
#14903=CARTESIAN_POINT('Origin',(44.3272645584124,-89.5,19.5));
#14904=CARTESIAN_POINT('Origin',(-32.5,-89.5,20.5));
#14905=CARTESIAN_POINT('',(-32.5,-90.,20.5));
#14906=CARTESIAN_POINT('',(-32.5,-89.5,20.));
#14907=CARTESIAN_POINT('Origin',(44.3272645584124,-89.5,17.8489128715187));
#14908=CARTESIAN_POINT('',(44.8272645584125,-89.5,17.8489128715187));
#14909=CARTESIAN_POINT('',(44.3272645584124,-90.,17.8489128715187));
#14910=CARTESIAN_POINT('Origin',(45.3272645584125,-45.,19.5));
#14911=CARTESIAN_POINT('',(45.3272645584125,-45.,20.));
#14912=CARTESIAN_POINT('',(44.8272645584125,-45.,19.5));
#14913=CARTESIAN_POINT('Origin',(64.5,-45.,20.5));
#14914=CARTESIAN_POINT('',(65.,-45.,20.5));
#14915=CARTESIAN_POINT('',(64.5,-45.,20.));
#14916=CARTESIAN_POINT('Origin',(64.5,-89.5,20.));
#14917=CARTESIAN_POINT('',(64.5,-90.,20.));
#14918=CARTESIAN_POINT('',(65.,-89.5,20.));
#14919=CARTESIAN_POINT('Origin',(-21.7129396307488,-89.5,16.1978257430375));
#14920=CARTESIAN_POINT('',(-21.7129396307488,-89.5,15.6978257430375));
#14921=CARTESIAN_POINT('',(-21.7129396307488,-90.,16.1978257430375));
#14922=CARTESIAN_POINT('Origin',(44.3272645584125,-90.,16.1978257430375));
#14923=CARTESIAN_POINT('',(44.3272645584125,-90.,15.6978257430375));
#14924=CARTESIAN_POINT('',(44.8272645584125,-90.,16.1978257430375));
#14925=CARTESIAN_POINT('Origin',(64.5,89.5,20.));
#14926=CARTESIAN_POINT('',(65.,89.5,20.));
#14927=CARTESIAN_POINT('',(64.5,90.,20.));
#14928=CARTESIAN_POINT('Origin',(64.5,-45.,31.5));
#14929=CARTESIAN_POINT('',(64.5,-45.,32.));
#14930=CARTESIAN_POINT('',(65.,-45.,31.5));
#14931=CARTESIAN_POINT('Origin',(-32.5,-89.5,31.5));
#14932=CARTESIAN_POINT('',(-32.5,-89.5,32.));
#14933=CARTESIAN_POINT('',(-32.5,-90.,31.5));
#14934=CARTESIAN_POINT('Origin',(21.0741207385024,-89.5,11.8489128715187));
#14935=CARTESIAN_POINT('',(21.5741207385024,-89.5,11.8489128715187));
#14936=CARTESIAN_POINT('',(21.0741207385024,-90.,11.8489128715187));
#14937=CARTESIAN_POINT('Origin',(22.0741207385024,-90.,15.1978257430375));
#14938=CARTESIAN_POINT('',(21.5741207385024,-90.,15.1978257430375));
#14939=CARTESIAN_POINT('',(22.0741207385024,-90.,15.6978257430375));
#14940=CARTESIAN_POINT('Origin',(32.5,89.5,31.5));
#14941=CARTESIAN_POINT('',(32.5,89.5,32.));
#14942=CARTESIAN_POINT('',(32.5,90.,31.5));
#14943=CARTESIAN_POINT('Origin',(-64.5,45.,31.5));
#14944=CARTESIAN_POINT('',(-64.5,45.,32.));
#14945=CARTESIAN_POINT('',(-65.,45.,31.5));
#14946=CARTESIAN_POINT('Origin',(-42.0226500362545,-89.5,4.19782574303749));
#14947=CARTESIAN_POINT('',(-42.0226500362545,-89.5,3.69782574303749));
#14948=CARTESIAN_POINT('',(-42.0226500362545,-90.,4.19782574303749));
#14949=CARTESIAN_POINT('Origin',(21.0741207385024,-90.,4.19782574303749));
#14950=CARTESIAN_POINT('',(21.0741207385024,-90.,3.69782574303749));
#14951=CARTESIAN_POINT('',(21.5741207385024,-90.,4.19782574303749));
#14952=CARTESIAN_POINT('Origin',(-64.5,45.,20.5));
#14953=CARTESIAN_POINT('',(-65.,45.,20.5));
#14954=CARTESIAN_POINT('',(-64.5,45.,20.));
#14955=CARTESIAN_POINT('Origin',(-18.545300072509,-89.5,17.8489128715187));
#14956=CARTESIAN_POINT('',(-19.045300072509,-89.5,17.8489128715187));
#14957=CARTESIAN_POINT('',(-18.545300072509,-90.,17.8489128715187));
#14958=CARTESIAN_POINT('Origin',(-18.545300072509,-90.,4.19782574303749));
#14959=CARTESIAN_POINT('',(-19.045300072509,-90.,4.19782574303749));
#14960=CARTESIAN_POINT('',(-18.545300072509,-90.,3.69782574303749));
#14961=CARTESIAN_POINT('Origin',(-23.0395928638606,-45.,19.5));
#14962=CARTESIAN_POINT('',(-23.0395928638606,-45.,20.));
#14963=CARTESIAN_POINT('',(-22.6860394732673,-45.,19.1464466094067));
#14964=CARTESIAN_POINT('Origin',(-45.5673301698183,-89.5,16.1978257430375));
#14965=CARTESIAN_POINT('',(-45.5673301698183,-89.5,15.6978257430375));
#14966=CARTESIAN_POINT('',(-45.5673301698183,-90.,16.1978257430375));
#14967=CARTESIAN_POINT('Origin',(-19.545300072509,-90.,15.1978257430375));
#14968=CARTESIAN_POINT('',(-19.545300072509,-90.,15.6978257430375));
#14969=CARTESIAN_POINT('',(-19.045300072509,-90.,15.1978257430375));
#14970=CARTESIAN_POINT('Origin',(0.229188828587721,89.5,41.3545681300752));
#14971=CARTESIAN_POINT('',(-0.124364562005555,89.5,41.7081215206685));
#14972=CARTESIAN_POINT('',(0.229188828587721,90.,41.3545681300752));
#14973=CARTESIAN_POINT('Origin',(-24.92755355845,-90.,16.1978257430375));
#14974=CARTESIAN_POINT('',(-25.2811069490433,-90.,16.5513791336308));
#14975=CARTESIAN_POINT('',(-24.92755355845,-90.,15.6978257430375));
#14976=CARTESIAN_POINT('Origin',(-65.,-90.,20.));
#14977=CARTESIAN_POINT('Origin',(-21.8324860826741,-90.,20.));
#14978=CARTESIAN_POINT('Origin',(0.,0.,20.));
#14979=CARTESIAN_POINT('Origin',(-65.,90.,20.));
#14980=CARTESIAN_POINT('Origin',(0.,0.,20.));
#14981=CARTESIAN_POINT('Origin',(44.8272645584125,-90.,15.6978257430375));
#14982=CARTESIAN_POINT('Origin',(65.,-90.,20.));
#14983=CARTESIAN_POINT('Origin',(21.5741207385024,-90.,15.6978257430375));
#14984=CARTESIAN_POINT('Origin',(0.,0.,32.));
#14985=CARTESIAN_POINT('Origin',(21.5741207385024,-90.,3.69782574303749));
#14986=CARTESIAN_POINT('Origin',(-19.045300072509,-90.,3.69782574303749));
#14987=CARTESIAN_POINT('Origin',(-19.045300072509,-90.,15.6978257430375));
#14988=CARTESIAN_POINT('Origin',(-26.1346603396366,-90.,15.6978257430375));
#14989=CARTESIAN_POINT('Origin',(65.,90.,20.));
#17816=UNCERTAINTY_MEASURE_WITH_UNIT(LENGTH_MEASURE(0.01),#17837,
'DISTANCE_ACCURACY_VALUE',
'Maximum model space distance between geometric entities at asserted c
onnectivities');
#17824=UNCERTAINTY_MEASURE_WITH_UNIT(LENGTH_MEASURE(0.01),#17837,
'DISTANCE_ACCURACY_VALUE',
'Maximum model space distance between geometric entities at asserted c
onnectivities');
#17828=(
GEOMETRIC_REPRESENTATION_CONTEXT(3)
GLOBAL_UNCERTAINTY_ASSIGNED_CONTEXT((#17816))
GLOBAL_UNIT_ASSIGNED_CONTEXT((#17837,#17839,#17840))
REPRESENTATION_CONTEXT('','3D')
);
#17836=(
GEOMETRIC_REPRESENTATION_CONTEXT(3)
GLOBAL_UNCERTAINTY_ASSIGNED_CONTEXT((#17824))
GLOBAL_UNIT_ASSIGNED_CONTEXT((#17837,#17839,#17840))
REPRESENTATION_CONTEXT('','3D')
);
#17837=(
LENGTH_UNIT()
NAMED_UNIT(*)
SI_UNIT(.MILLI.,.METRE.)
);
#17839=(
NAMED_UNIT(*)
PLANE_ANGLE_UNIT()
SI_UNIT($,.RADIAN.)
);
#17840=(
NAMED_UNIT(*)
SI_UNIT($,.STERADIAN.)
SOLID_ANGLE_UNIT()
);
#17844=SHAPE_DEFINITION_REPRESENTATION(#17855,#17876);
#17855=PRODUCT_DEFINITION_SHAPE('',$,#17888);
#17876=SHAPE_REPRESENTATION('',(#9932),#17828);
#17884=PRODUCT_DEFINITION_CONTEXT('part definition',#17919,'design');
#17888=PRODUCT_DEFINITION('Moving_Carriage_02','Moving_Carriage_02',#17899,
#17884);
#17899=PRODUCT_DEFINITION_FORMATION('',$,#17924);
#17919=APPLICATION_CONTEXT(
'Core Data for Automotive Mechanical Design Process');
#17920=PRODUCT_CONTEXT('part definition',#17919,'mechanical');
#17924=PRODUCT('Moving_Carriage_02','Moving_Carriage_02',$,(#17920));
#17960=COLOUR_RGB('Sky Blue',0.24,0.69,0.87);
#17961=FILL_AREA_STYLE_COLOUR('',#17960);
#17962=FILL_AREA_STYLE('',(#17961));
#17963=SURFACE_STYLE_FILL_AREA(#17962);
#17964=SURFACE_SIDE_STYLE('',(#17963));
#17965=SURFACE_STYLE_USAGE(.BOTH.,#17964);
#17966=PRESENTATION_STYLE_ASSIGNMENT((#17965));
ENDSEC;
END-ISO-10303-21;
